ISO-10303-21;
HEADER;
FILE_DESCRIPTION (('STEP AP214'),
    '1' );
FILE_NAME ('hex flange bolt small_iso_ISO 4162 - M5 x 25 x 16-N.step',
    '2026-09-24T10:26:00',
    ( '' ),
    ( '' ),
    'SwSTEP 2.0',
    'SolidWorks 2026',
    '' );
FILE_SCHEMA (( 'AUTOMOTIVE_DESIGN' ));
ENDSEC;

DATA;
#31=CARTESIAN_POINT ( 'NONE',  ( 0.1217565302851067177, -3.710888496608912845, 0.5725525826504656024 ) ) ;
#40=CARTESIAN_POINT ( 'NONE',  ( 4.086376042167607636, -4.082715877136871008, 0.07147133206917684334 ) ) ;
#44=CARTESIAN_POINT ( 'NONE',  ( 4.050823680195247078, 3.779313952391380127, -0.5899027668435176119 ) ) ;
#54=ORIENTED_EDGE ( 'NONE', *, *, #9609, .T. ) ;
#76=CARTESIAN_POINT ( 'NONE',  ( 4.142654963991838635, -2.035398498734361183, 3.525413613457314188 ) ) ;
#79=VERTEX_POINT ( 'NONE', #5274 ) ;
#117=DIRECTION ( 'NONE',  ( -2.273843122241288438E-18, -5.551115123125783935E-17, -1.000000000000000000 ) ) ;
#119=CARTESIAN_POINT ( 'NONE',  ( 4.071447262713911996, -2.020725942163681399, 3.499999999999989342 ) ) ;
#132=DIRECTION ( 'NONE',  ( -1.000000000000000000, -3.286707217423839940E-17, -2.273843122241288053E-18 ) ) ;
#167=CARTESIAN_POINT ( 'NONE',  ( 0.000000000000000000, 0.000000000000000000, 0.000000000000000000 ) ) ;
#172=VERTEX_POINT ( 'NONE', #3659 ) ;
#182=CARTESIAN_POINT ( 'NONE',  ( 0.000000000000000000, 0.000000000000000000, 0.000000000000000000 ) ) ;
#204=CARTESIAN_POINT ( 'NONE',  ( 4.071447262713911996, 2.020725942163681399, -3.499999999999996003 ) ) ;
#238=ORIENTED_EDGE ( 'NONE', *, *, #350, .F. ) ;
#247=CARTESIAN_POINT ( 'NONE',  ( 4.175326769692832229, -2.060699556488890138, -3.569236330973504678 ) ) ;
#251=DIRECTION ( 'NONE',  ( 2.732679788978641511E-17, 0.8660254037844375974, -0.5000000000000019984 ) ) ;
#265=EDGE_LOOP ( 'NONE', ( #8330, #2797, #508, #8925 ) ) ;
#269=VERTEX_POINT ( 'NONE', #12870 ) ;
#279=CARTESIAN_POINT ( 'NONE',  ( 0.2174200650117580069, 3.876582599186215727, 0.2855619784720741516 ) ) ;
#323=CARTESIAN_POINT ( 'NONE',  ( 4.142654963991838635, -2.035398498734360739, -3.525413613457307083 ) ) ;
#343=CLOSED_SHELL ( 'NONE', ( #348, #10277, #10610, #2946, #4930, #5603, #8583, #3122, #8964, #584, #2814, #2804, #5042, #11746, #8231, #7567, #9589, #9255, #10929, #2822, #4189, #8522, #2178, #12387, #5966, #9430, #5583, #8276, #5909 ) ) ;
#348=ADVANCED_FACE ( 'NONE', ( #1821 ), #11776, .T. ) ;
#349=CARTESIAN_POINT ( 'NONE',  ( 5.599999999999994316, -4.041451884327377009, 0.000000000000000000 ) ) ;
#350=EDGE_CURVE ( 'NONE', #1315, #10506, #376, .T. ) ;
#357=ORIENTED_EDGE ( 'NONE', *, *, #6598, .T. ) ;
#368=CARTESIAN_POINT ( 'NONE',  ( 1.671902908347949033E-15, 2.686816014504571193, 2.346298152288376127 ) ) ;
#376=B_SPLINE_CURVE_WITH_KNOTS ( 'NONE', 3,
 ( #7503, #2032, #11022, #6628, #11096, #11995 ),
 .UNSPECIFIED., .F., .F.,
 ( 4, 2, 4 ),
 ( 0.01308430721348208085, 0.01410661710602280003, 0.01512892699856351920 ),
 .UNSPECIFIED. ) ;
#392=CARTESIAN_POINT ( 'NONE',  ( 4.082498951862935321, 2.020725942163681399, 3.499999999999996003 ) ) ;
#411=EDGE_LOOP ( 'NONE', ( #1168, #3751, #5257, #2145 ) ) ;
#415=PRODUCT_DEFINITION_SHAPE ( 'NONE', 'NONE',  #11244 ) ;
#419=CARTESIAN_POINT ( 'NONE',  ( 4.175813232069169878, 2.061359961916364725, -3.570380186727395433 ) ) ;
#440=AXIS2_PLACEMENT_3D ( 'NONE', #7787, #251, #5655 ) ;
#443=CARTESIAN_POINT ( 'NONE',  ( 0.3126073911696169993, -2.020725942163681399, 3.499999999999989342 ) ) ;
#452=CARTESIAN_POINT ( 'NONE',  ( 4.071447262713911996, -4.041451884327377009, 0.000000000000000000 ) ) ;
#457=VECTOR ( 'NONE', #1303, 1000.000000000000000 ) ;
#477=ORIENTED_EDGE ( 'NONE', *, *, #13369, .F. ) ;
#486=EDGE_LOOP ( 'NONE', ( #3660, #11536, #1623, #8148, #13235 ) ) ;
#508=ORIENTED_EDGE ( 'NONE', *, *, #6035, .F. ) ;
#517=CARTESIAN_POINT ( 'NONE',  ( 4.071447262713911996, -2.020725942163681399, -3.500000000000010214 ) ) ;
#541=ORIENTED_EDGE ( 'NONE', *, *, #11559, .T. ) ;
#584=ADVANCED_FACE ( 'NONE', ( #10851 ), #6393, .T. ) ;
#603=DIRECTION ( 'NONE',  ( 0.000000000000000000, -5.551115123125782702E-17, -1.000000000000000000 ) ) ;
#624=CARTESIAN_POINT ( 'NONE',  ( 0.02993401039713497816, -3.373851915354613151, -1.156317065392235222 ) ) ;
#646=ORIENTED_EDGE ( 'NONE', *, *, #11385, .F. ) ;
#665=PLANE ( 'NONE',  #4214 ) ;
#673=CARTESIAN_POINT ( 'NONE',  ( 3.950241966888151879, -3.393956070637468958, 1.121495646998917017 ) ) ;
#712=CARTESIAN_POINT ( 'NONE',  ( 3.878096787214415198, 2.680238624820971083, -2.357690525401547443 ) ) ;
#728=CONICAL_SURFACE ( 'NONE', #12412, 2.054999999999999716, 0.7853981633974428389 ) ;
#750=AXIS2_PLACEMENT_3D ( 'NONE', #4185, #13245, #6639 ) ;
#759=UNCERTAINTY_MEASURE_WITH_UNIT (LENGTH_MEASURE( 1.000000000000000082E-05 ), #7893, 'distance_accuracy_value', 'NONE');
#761=LINE ( 'NONE', #12029, #4486 ) ;
#766=CARTESIAN_POINT ( 'NONE',  ( 30.60000000000001563, 1.140754157802348188E-16, 2.054999999999999716 ) ) ;
#771=ORIENTED_EDGE ( 'NONE', *, *, #1381, .F. ) ;
#776=CARTESIAN_POINT ( 'NONE',  ( 5.599999999999994316, 4.041451884327390331, 0.000000000000000000 ) ) ;
#782=CARTESIAN_POINT ( 'NONE',  ( 3.806834918298607651, 8.673617379884035472E-16, -3.499999999999975131 ) ) ;
#786=CARTESIAN_POINT ( 'NONE',  ( 4.124214193018064911, -4.056676826581889550, -6.938408812827713022E-15 ) ) ;
#790=CARTESIAN_POINT ( 'NONE',  ( 3.972058292797703949, 0.6948821373597541262, 3.565770528409232920 ) ) ;
#796=EDGE_CURVE ( 'NONE', #3727, #13520, #8809, .T. ) ;
#797=EDGE_LOOP ( 'NONE', ( #4889, #11976, #11139, #14129 ) ) ;
#799=EDGE_CURVE ( 'NONE', #14126, #11064, #3187, .T. ) ;
#813=CARTESIAN_POINT ( 'NONE',  ( 0.2174200650117486533, 2.185595227304854227, -3.214438021527926459 ) ) ;
#822=CARTESIAN_POINT ( 'NONE',  ( 0.2174200650117520395, -3.876582599186206846, -0.2855619784720702103 ) ) ;
#825=CARTESIAN_POINT ( 'NONE',  ( 4.093692494532780835, 4.043567292011559289, -1.387813195790392893E-14 ) ) ;
#841=ORIENTED_EDGE ( 'NONE', *, *, #13660, .T. ) ;
#879=AXIS2_PLACEMENT_3D ( 'NONE', #5715, #4377, #11362 ) ;
#909=CARTESIAN_POINT ( 'NONE',  ( 3.948103430090711186, -3.379418997638564459, -1.146674596026800330 ) ) ;
#933=CARTESIAN_POINT ( 'NONE',  ( 3.972066048304740082, -2.740530939476243155, 2.384802634787796194 ) ) ;
#1004=CARTESIAN_POINT ( 'NONE',  ( 4.033895293470907362, 1.419609371825386823, -3.499999999999992450 ) ) ;
#1018=AXIS2_PLACEMENT_3D ( 'NONE', #8546, #10822, #12127 ) ;
#1045=CARTESIAN_POINT ( 'NONE',  ( 0.000000000000000000, 0.000000000000000000, -3.500000000000010214 ) ) ;
#1053=CARTESIAN_POINT ( 'NONE',  ( 4.071447262713911996, -2.020725942163681399, -3.500000000000010214 ) ) ;
#1063=CARTESIAN_POINT ( 'NONE',  ( 3.974175853609971831, -2.726149789692694281, -2.409821656223178454 ) ) ;
#1065=CARTESIAN_POINT ( 'NONE',  ( 0.000000000000000000, 0.000000000000000000, 0.000000000000000000 ) ) ;
#1077=DIRECTION ( 'NONE',  ( 2.273843122241288438E-18, 5.551115123125782702E-17, 1.000000000000000000 ) ) ;
#1079=CARTESIAN_POINT ( 'NONE',  ( 5.599999999999994316, 2.020725942163681399, -3.499999999999996003 ) ) ;
#1083=DIRECTION ( 'NONE',  ( -1.000000000000000000, -3.286707217423839940E-17, -2.273843122241288053E-18 ) ) ;
#1103=VERTEX_POINT ( 'NONE', #9236 ) ;
#1104=ORIENTED_EDGE ( 'NONE', *, *, #11095, .T. ) ;
#1118=CARTESIAN_POINT ( 'NONE',  ( 3.972709601346605890, -3.429395227388305933, -1.191688283765312217 ) ) ;
#1133=PLANE ( 'NONE',  #879 ) ;
#1158=CARTESIAN_POINT ( 'NONE',  ( 4.114405500665259119, -2.025575754679708407, 3.508400121684919881 ) ) ;
#1168=ORIENTED_EDGE ( 'NONE', *, *, #4608, .T. ) ;
#1170=EDGE_CURVE ( 'NONE', #14055, #6673, #761, .T. ) ;
#1212=CARTESIAN_POINT ( 'NONE',  ( 5.599999999999994316, 0.000000000000000000, 0.000000000000000000 ) ) ;
#1269=CARTESIAN_POINT ( 'NONE',  ( 4.175813232069169878, 2.061359961916364725, -3.570380186727395433 ) ) ;
#1274=CARTESIAN_POINT ( 'NONE',  ( 4.158413352280787123, -2.044871626972824430, -3.541821552872956413 ) ) ;
#1291=DIRECTION ( 'NONE',  ( -1.000000000000000000, -3.286707217423839940E-17, -2.273843122241288053E-18 ) ) ;
#1296=AXIS2_PLACEMENT_3D ( 'NONE', #10325, #3832, #2495 ) ;
#1303=DIRECTION ( 'NONE',  ( -1.000000000000000000, -3.286707217423839940E-17, -2.273843122241288053E-18 ) ) ;
#1306=CARTESIAN_POINT ( 'NONE',  ( 30.15499999999998693, 0.000000000000000000, 0.000000000000000000 ) ) ;
#1315=VERTEX_POINT ( 'NONE', #1045 ) ;
#1364=CARTESIAN_POINT ( 'NONE',  ( 3.951447005078475350, 2.357513599190963927, 2.916666666666662078 ) ) ;
#1371=EDGE_CURVE ( 'NONE', #6548, #8214, #1905, .T. ) ;
#1372=DIRECTION ( 'NONE',  ( 1.000000000000000000, 3.286707217423839940E-17, 2.273843122241288053E-18 ) ) ;
#1381=EDGE_CURVE ( 'NONE', #1103, #1315, #4919, .T. ) ;
#1399=ORIENTED_EDGE ( 'NONE', *, *, #6270, .T. ) ;
#1406=CARTESIAN_POINT ( 'NONE',  ( 4.142654963991843076, 2.035398498734334538, 3.525413613457302198 ) ) ;
#1428=ORIENTED_EDGE ( 'NONE', *, *, #12406, .T. ) ;
#1476=SURFACE_STYLE_USAGE ( .BOTH. , #6223 ) ;
#1514=CARTESIAN_POINT ( 'NONE',  ( 0.000000000000000000, 0.000000000000000000, -3.500000000000010214 ) ) ;
#1521=CARTESIAN_POINT ( 'NONE',  ( 4.082498951862935321, 2.020725942163680511, -3.499999999999997780 ) ) ;
#1528=CARTESIAN_POINT ( 'NONE',  ( 0.000000000000000000, -3.031088913245536087, 1.750000000000001554 ) ) ;
#1533=CARTESIAN_POINT ( 'NONE',  ( 4.175813232069169878, -4.122719923832743660, -6.938893903907228378E-15 ) ) ;
#1562=CARTESIAN_POINT ( 'NONE',  ( 0.3126073911696169993, 2.020725942163681399, -3.499999999999996003 ) ) ;
#1615=CIRCLE ( 'NONE', #7686, 2.054999999999999716 ) ;
#1616=( NAMED_UNIT ( * ) SI_UNIT ( $, .STERADIAN. ) SOLID_ANGLE_UNIT ( ) );
#1623=ORIENTED_EDGE ( 'NONE', *, *, #14426, .T. ) ;
#1624=EDGE_CURVE ( 'NONE', #7658, #7309, #5463, .T. ) ;
#1665=DIRECTION ( 'NONE',  ( 0.000000000000000000, 5.551115123125782702E-17, 1.000000000000000000 ) ) ;
#1694=ORIENTED_EDGE ( 'NONE', *, *, #9360, .T. ) ;
#1713=CARTESIAN_POINT ( 'NONE',  ( 30.60000000000001563, 0.000000000000000000, 0.000000000000000000 ) ) ;
#1715=CARTESIAN_POINT ( 'NONE',  ( 4.175326769692884632, 4.121399112977849555, -8.369832099842142803E-15 ) ) ;
#1730=EDGE_CURVE ( 'NONE', #12256, #3727, #4276, .T. ) ;
#1740=VECTOR ( 'NONE', #9766, 1000.000000000000114 ) ;
#1763=CARTESIAN_POINT ( 'NONE',  ( 4.033901012034863065, -3.740908793663352938, 0.5205559028927786436 ) ) ;
#1782=CARTESIAN_POINT ( 'NONE',  ( 4.175813232069169878, -4.122719923832743660, -6.938893903907228378E-15 ) ) ;
#1806=( BOUNDED_SURFACE ( )  B_SPLINE_SURFACE ( 3, 2, ( 
 ( #10816, #6765, #4460 ),
 ( #5527, #13516, #12198 ),
 ( #8888, #9025, #12339 ),
 ( #3424, #12272, #7862 ),
 ( #6845, #7637, #3358 ),
 ( #3495, #3279, #13386 ) ),
 .UNSPECIFIED., .F., .F., .T. ) 
 B_SPLINE_SURFACE_WITH_KNOTS ( ( 4, 2, 4 ),
 ( 3, 3 ),
 ( 0.01651999345535504898, 0.01858032176739834312, 0.02064065007944163380 ),
 ( 0.000000000000000000, 1.000000000000000000 ),
 .UNSPECIFIED. ) 
 GEOMETRIC_REPRESENTATION_ITEM ( )  RATIONAL_B_SPLINE_SURFACE ( (
 ( 1.000000000000000000, 0.8047781103519393575, 1.000000000000000000),
 ( 1.000000000000000000, 0.8123785825598874855, 1.000000000000000000),
 ( 1.000000000000000000, 0.8190671539795569833, 1.000000000000000000),
 ( 1.000000000000000000, 0.8192352254827578451, 1.000000000000000000),
 ( 1.000000000000000000, 0.8126129677217079905, 1.000000000000000000),
 ( 1.000000000000000000, 0.8047712537969728963, 1.000000000000000000) ) ) 
 REPRESENTATION_ITEM ( '' )  SURFACE ( )  );
#1816=EDGE_CURVE ( 'NONE', #2047, #8757, #2506, .T. ) ;
#1821=FACE_OUTER_BOUND ( 'NONE', #411, .T. ) ;
#1832=DIRECTION ( 'NONE',  ( -1.000000000000000000, -3.286707217423839940E-17, -2.273843122241288053E-18 ) ) ;
#1870=FACE_OUTER_BOUND ( 'NONE', #486, .T. ) ;
#1873=EDGE_CURVE ( 'NONE', #269, #11894, #10364, .T. ) ;
#1905=CIRCLE ( 'NONE', #9829, 0.4999999999999978351 ) ;
#1913=MECHANICAL_DESIGN_GEOMETRIC_PRESENTATION_REPRESENTATION('',(#8198),#10307);
#1918=CARTESIAN_POINT ( 'NONE',  ( -1.295960409299079124E-15, 0.3423821193476913050, 3.499999999999996003 ) ) ;
#1929=ORIENTED_EDGE ( 'NONE', *, *, #7016, .T. ) ;
#1946=ORIENTED_EDGE ( 'NONE', *, *, #6197, .F. ) ;
#1952=DIRECTION ( 'NONE',  ( -1.000000000000000000, -3.286707217423839940E-17, -2.273843122241288053E-18 ) ) ;
#1959=B_SPLINE_CURVE_WITH_KNOTS ( 'NONE', 3,
 ( #12836, #13066, #825, #11739, #2968, #13938, #2820, #3847, #10563, #4143, #7259, #6385, #10640, #1715, #9690, #11656 ),
 .UNSPECIFIED., .F., .F.,
 ( 4, 3, 3, 3, 3, 4 ),
 ( 0.000000000000000000, 3.315506744709155554E-05, 6.608280158698769959E-05, 0.0001026520855291340468, 0.0001376952025664801528, 0.0001398064759190615887 ),
 .UNSPECIFIED. ) ;
#1965=DIRECTION ( 'NONE',  ( -1.000000000000000000, -3.286707217423839940E-17, -2.273843122241288053E-18 ) ) ;
#1984=CARTESIAN_POINT ( 'NONE',  ( 4.170895651974822371, -2.054890354522667995, 3.559174498016340227 ) ) ;
#1989=CARTESIAN_POINT ( 'NONE',  ( 0.3126073911696169993, 2.020725942163681399, -3.499999999999996003 ) ) ;
#1997=MANIFOLD_SOLID_BREP ( 'FlangeHexFillet', #343 ) ;
#1999=EDGE_CURVE ( 'NONE', #11064, #10506, #2413, .T. ) ;
#2020=ORIENTED_EDGE ( 'NONE', *, *, #6153, .F. ) ;
#2021=CARTESIAN_POINT ( 'NONE',  ( 3.878096787214416530, -3.381939201670113526, -1.142309474598453667 ) ) ;
#2032=CARTESIAN_POINT ( 'NONE',  ( -2.134523027080836066E-15, -0.3420925509381486651, -3.499999999999995115 ) ) ;
#2047=VERTEX_POINT ( 'NONE', #5109 ) ;
#2091=CARTESIAN_POINT ( 'NONE',  ( 4.033901012036043454, -2.321269032826913659, -2.979444097106994427 ) ) ;
#2094=CARTESIAN_POINT ( 'NONE',  ( 4.086376210449946811, 2.103254844323302564, 3.499999999999992450 ) ) ;
#2102=ORIENTED_EDGE ( 'NONE', *, *, #13571, .F. ) ;
#2105=AXIS2_PLACEMENT_3D ( 'NONE', #3365, #132, #1077 ) ;
#2116=CARTESIAN_POINT ( 'NONE',  ( 4.151274195509661702, 2.039912954708745563, -3.533232880573503376 ) ) ;
#2119=ORIENTED_EDGE ( 'NONE', *, *, #1730, .F. ) ;
#2127=CONICAL_SURFACE ( 'NONE', #3306, 3.499999999999999112, 1.047197551196600296 ) ;
#2141=AXIS2_PLACEMENT_3D ( 'NONE', #7308, #12969, #3815 ) ;
#2145=ORIENTED_EDGE ( 'NONE', *, *, #10928, .F. ) ;
#2150=B_SPLINE_CURVE_WITH_KNOTS ( 'NONE', 3,
 ( #7764, #12238, #7601, #12085 ),
 .UNSPECIFIED., .F., .F.,
 ( 4, 4 ),
 ( 2.380739282789443030E-07, 0.002044882221487529742 ),
 .UNSPECIFIED. ) ;
#2172=CARTESIAN_POINT ( 'NONE',  ( 4.158921784487740858, 2.089935040870093630, 3.499999999999992006 ) ) ;
#2178=ADVANCED_FACE ( 'NONE', ( #10679 ), #665, .F. ) ;
#2240=FACE_BOUND ( 'NONE', #9215, .T. ) ;
#2243=CARTESIAN_POINT ( 'NONE',  ( 3.951447005078477126, 1.347150628109121673, 3.499999999999996447 ) ) ;
#2270=VERTEX_POINT ( 'NONE', #7442 ) ;
#2288=( LENGTH_UNIT ( ) NAMED_UNIT ( * ) SI_UNIT ( .MILLI., .METRE. ) );
#2292=EDGE_LOOP ( 'NONE', ( #3899, #7819, #12147, #238, #10818 ) ) ;
#2293=CARTESIAN_POINT ( 'NONE',  ( 3.951447005078475350, -2.357513599190963927, -2.916666666666674512 ) ) ;
#2303=CIRCLE ( 'NONE', #6487, 2.499999999999999112 ) ;
#2304=CARTESIAN_POINT ( 'NONE',  ( 3.972066048304813801, -3.435565134476607163, -1.180968096049836769 ) ) ;
#2306=DIRECTION ( 'NONE',  ( -2.273843122241288438E-18, -5.551115123125783935E-17, -1.000000000000000000 ) ) ;
#2319=B_SPLINE_CURVE_WITH_KNOTS ( 'NONE', 3,
 ( #2375, #4451, #13507, #6534, #4647 ),
 .UNSPECIFIED., .F., .F.,
 ( 4, 1, 4 ),
 ( 0.000000000000000000, 0.002020725942163693108, 0.004041451884327386217 ),
 .UNSPECIFIED. ) ;
#2325=PLANE ( 'NONE',  #5561 ) ;
#2329=CARTESIAN_POINT ( 'NONE',  ( 3.878096787214413421, -2.680238624820956872, 2.357690525401561210 ) ) ;
#2354=( BOUNDED_SURFACE ( )  B_SPLINE_SURFACE ( 3, 2, ( 
 ( #12419, #3429, #5469 ),
 ( #5396, #1004, #6630 ),
 ( #9865, #3212, #5602 ),
 ( #13392, #13460, #2394 ),
 ( #5672, #7872, #10074 ),
 ( #8827, #13309, #8760 ) ),
 .UNSPECIFIED., .F., .F., .T. ) 
 B_SPLINE_SURFACE_WITH_KNOTS ( ( 4, 2, 4 ),
 ( 3, 3 ),
 ( 0.01652267773200353021, 0.01858309280828997906, 0.02064350788457643138 ),
 ( 0.000000000000000000, 1.000000000000000000 ),
 .UNSPECIFIED. ) 
 GEOMETRIC_REPRESENTATION_ITEM ( )  RATIONAL_B_SPLINE_SURFACE ( (
 ( 1.000000000000000000, 0.8047780975688292315, 1.000000000000000000),
 ( 1.000000000000000000, 0.8123789546319812871, 1.000000000000000000),
 ( 1.000000000000000000, 0.8190677982995108186, 1.000000000000000000),
 ( 1.000000000000000000, 0.8192346069545793918, 1.000000000000000000),
 ( 1.000000000000000000, 0.8126126759773680819, 1.000000000000000000),
 ( 1.000000000000000000, 0.8047712639311999094, 1.000000000000000000) ) ) 
 REPRESENTATION_ITEM ( '' )  SURFACE ( )  );
#2357=CARTESIAN_POINT ( 'NONE',  ( 4.050880675075964277, -1.379097446046169795, -3.567934390854442306 ) ) ;
#2375=CARTESIAN_POINT ( 'NONE',  ( 4.071447262713911996, -4.041451884327377009, 0.000000000000000000 ) ) ;
#2394=CARTESIAN_POINT ( 'NONE',  ( 3.972073812946703253, -0.6951863858504719884, -3.565770933504595952 ) ) ;
#2413=LINE ( 'NONE', #11334, #457 ) ;
#2443=CARTESIAN_POINT ( 'NONE',  ( 4.175075985190068728, 2.060370777630132544, 3.568666869285544330 ) ) ;
#2444=CARTESIAN_POINT ( 'NONE',  ( 4.114405500665256454, -2.025575754679707519, -3.508400121684932760 ) ) ;
#2495=DIRECTION ( 'NONE',  ( 3.286707217423841172E-17, 1.000000000000000000, -5.551115123125782702E-17 ) ) ;
#2506=B_SPLINE_CURVE_WITH_KNOTS ( 'NONE', 3,
 ( #8565, #1918, #2880, #6064, #7324, #3969 ),
 .UNSPECIFIED., .F., .F.,
 ( 4, 2, 4 ),
 ( 0.005852013098461913629, 0.006875955139453155188, 0.007899897180444396746 ),
 .UNSPECIFIED. ) ;
#2512=AXIS2_PLACEMENT_3D ( 'NONE', #7495, #1965, #1665 ) ;
#2516=DIRECTION ( 'NONE',  ( 0.000000000000000000, 5.551115123125782702E-17, 1.000000000000000000 ) ) ;
#2518=FACE_OUTER_BOUND ( 'NONE', #7435, .T. ) ;
#2531=AXIS2_PLACEMENT_3D ( 'NONE', #182, #13379, #12335 ) ;
#2533=B_SPLINE_CURVE_WITH_KNOTS ( 'NONE', 3,
 ( #7949, #1364, #10219, #12429, #2548 ),
 .UNSPECIFIED., .F., .F.,
 ( 4, 1, 4 ),
 ( 0.000000000000000000, 0.002020725942163691807, 0.004041451884327383615 ),
 .UNSPECIFIED. ) ;
#2534=CARTESIAN_POINT ( 'NONE',  ( 0.000000000000000000, 0.000000000000000000, 0.000000000000000000 ) ) ;
#2538=ORIENTED_EDGE ( 'NONE', *, *, #13660, .F. ) ;
#2548=CARTESIAN_POINT ( 'NONE',  ( 4.071447262713911996, 4.041451884327390331, 0.000000000000000000 ) ) ;
#2549=CARTESIAN_POINT ( 'NONE',  ( 0.3126073911696169993, 2.020725942163681399, 3.499999999999996003 ) ) ;
#2551=ORIENTED_EDGE ( 'NONE', *, *, #3641, .T. ) ;
#2568=ORIENTED_EDGE ( 'NONE', *, *, #1170, .T. ) ;
#2594=ORIENTED_EDGE ( 'NONE', *, *, #4608, .F. ) ;
#2604=DIRECTION ( 'NONE',  ( 1.000000000000000000, 3.286707217423839940E-17, 2.273843122241288053E-18 ) ) ;
#2610=CARTESIAN_POINT ( 'NONE',  ( 0.3126073911696169993, 2.020725942163681399, -3.499999999999996003 ) ) ;
#2618=CARTESIAN_POINT ( 'NONE',  ( 0.3126073911696169993, 4.041451884327390331, 0.000000000000000000 ) ) ;
#2645=EDGE_LOOP ( 'NONE', ( #2594, #11262 ) ) ;
#2648=EDGE_LOOP ( 'NONE', ( #7129, #6996, #1399, #13359, #7830, #4340, #3185 ) ) ;
#2653=B_SPLINE_CURVE_WITH_KNOTS ( 'NONE', 3,
 ( #3181, #11137, #6444, #12097, #5504, #9972 ),
 .UNSPECIFIED., .F., .F.,
 ( 4, 2, 4 ),
 ( 0.000000000000000000, 0.002086519881787261485, 0.004173039763574522970 ),
 .UNSPECIFIED. ) ;
#2654=PRESENTATION_STYLE_ASSIGNMENT (( #1476 ) ) ;
#2669=CARTESIAN_POINT ( 'NONE',  ( 4.104070371397483541, -2.023683613428362005, -3.505122836902505146 ) ) ;
#2710=CONICAL_SURFACE ( 'NONE', #10879, 3.499999999999999112, 1.047197551196600296 ) ;
#2728=FILL_AREA_STYLE ('',( #12662 ) ) ;
#2744=CYLINDRICAL_SURFACE ( 'NONE', #13264, 2.499999999999999112 ) ;
#2758=CARTESIAN_POINT ( 'NONE',  ( 5.099999999999993427, 3.481583491540829278E-16, -5.200000000000001066 ) ) ;
#2759=ORIENTED_EDGE ( 'NONE', *, *, #6035, .T. ) ;
#2768=EDGE_CURVE ( 'NONE', #13171, #14126, #7895, .T. ) ;
#2775=CARTESIAN_POINT ( 'NONE',  ( 4.104070371397483541, 2.023683613428362005, -3.505122836902505146 ) ) ;
#2784=EDGE_LOOP ( 'NONE', ( #6969, #8666, #10622, #8524, #1694, #54, #9238 ) ) ;
#2785=CIRCLE ( 'NONE', #8372, 5.200000000000001066 ) ;
#2797=ORIENTED_EDGE ( 'NONE', *, *, #7441, .F. ) ;
#2803=( LENGTH_UNIT ( ) NAMED_UNIT ( * ) SI_UNIT ( .MILLI., .METRE. ) );
#2804=ADVANCED_FACE ( 'NONE', ( #9993 ), #6736, .T. ) ;
#2814=ADVANCED_FACE ( 'NONE', ( #12474 ), #4454, .F. ) ;
#2820=CARTESIAN_POINT ( 'NONE',  ( 4.132952817037849336, 4.063368025374519910, -6.938893903907228378E-15 ) ) ;
#2822=ADVANCED_FACE ( 'NONE', ( #10059 ), #3349, .F. ) ;
#2841=VERTEX_POINT ( 'NONE', #9093 ) ;
#2843=CARTESIAN_POINT ( 'NONE',  ( 4.180231891692620216, 4.134807952925580565, 0.02076457676760649559 ) ) ;
#2870=CARTESIAN_POINT ( 'NONE',  ( 3.961551342853563806, -3.742715940867795688, 0.5174258321190287058 ) ) ;
#2880=CARTESIAN_POINT ( 'NONE',  ( 0.03027795055833587892, 0.6888063905328651870, 3.499999999999996891 ) ) ;
#2890=APPLICATION_CONTEXT ( 'automotive_design' ) ;
#2893=EDGE_CURVE ( 'NONE', #10783, #14055, #2303, .T. ) ;
#2928=CARTESIAN_POINT ( 'NONE',  ( 4.180231680468786237, -2.085385483809543583, 3.570466434508598574 ) ) ;
#2934=SHAPE_REPRESENTATION ( 'hex flange bolt small_iso_ISO 4162 - M5 x 25 x 16-N', ( #11025 ), #10318 ) ;
#2946=ADVANCED_FACE ( 'NONE', ( #12839 ), #2744, .T. ) ;
#2959=CARTESIAN_POINT ( 'NONE',  ( 0.000000000000000000, 0.000000000000000000, 0.000000000000000000 ) ) ;
#2968=CARTESIAN_POINT ( 'NONE',  ( 4.114405500665252013, 4.051151509359440794, -1.387744507531641370E-14 ) ) ;
#2972=ORIENTED_EDGE ( 'NONE', *, *, #3550, .F. ) ;
#2974=ADVANCED_BREP_SHAPE_REPRESENTATION ( '', ( #1997, #11025 ), #10318 ) ;
#2987=CARTESIAN_POINT ( 'NONE',  ( 3.951447005078477126, -1.347150628109121007, -3.500000000000011546 ) ) ;
#2991=CARTESIAN_POINT ( 'NONE',  ( 4.175813232069169878, -4.122719923832743660, -6.938893903907228378E-15 ) ) ;
#3005=B_SPLINE_CURVE_WITH_KNOTS ( 'NONE', 3,
 ( #14462, #7788, #3630, #9094, #44, #13512 ),
 .UNSPECIFIED., .F., .F.,
 ( 4, 2, 4 ),
 ( 0.000000000000000000, 0.002086519881787259750, 0.004173039763574519501 ),
 .UNSPECIFIED. ) ;
#3014=DIRECTION ( 'NONE',  ( -1.446433017903773725E-17, -0.5000000000000003331, 0.8660254037844383745 ) ) ;
#3093=CIRCLE ( 'NONE', #8680, 2.499999999999999112 ) ;
#3107=DIRECTION ( 'NONE',  ( 1.000000000000000000, 3.286707217423839940E-17, 2.273843122241288053E-18 ) ) ;
#3122=ADVANCED_FACE ( 'NONE', ( #7255 ), #6077, .F. ) ;
#3130=EDGE_LOOP ( 'NONE', ( #2759, #11816, #4750, #10395, #6166 ) ) ;
#3136=CARTESIAN_POINT ( 'NONE',  ( 3.950241966888157652, -2.668221755853173338, -2.378504353001417826 ) ) ;
#3154=CARTESIAN_POINT ( 'NONE',  ( 4.175813232069169878, 4.122719923832743660, 0.000000000000000000 ) ) ;
#3155=PRODUCT_CONTEXT ( 'NONE', #2890, 'mechanical' ) ;
#3181=CARTESIAN_POINT ( 'NONE',  ( 4.175813232069169878, -2.061359961916364725, 3.570380186727409200 ) ) ;
#3185=ORIENTED_EDGE ( 'NONE', *, *, #8957, .T. ) ;
#3187=B_SPLINE_CURVE_WITH_KNOTS ( 'NONE', 3,
 ( #13292, #3268, #782, #2987, #7707 ),
 .UNSPECIFIED., .F., .F.,
 ( 4, 1, 4 ),
 ( 0.000000000000000000, 0.002020725942163690073, 0.004041451884327380145 ),
 .UNSPECIFIED. ) ;
#3212=CARTESIAN_POINT ( 'NONE',  ( 3.950233766685595338, 0.7256672287185880199, -3.500000000000147882 ) ) ;
#3215=B_SPLINE_CURVE_WITH_KNOTS ( 'NONE', 3,
 ( #443, #3886, #10236, #11625, #4896, #7080 ),
 .UNSPECIFIED., .F., .F.,
 ( 4, 2, 4 ),
 ( 0.003805861006858111961, 0.004828937052660012795, 0.005852013098461913629 ),
 .UNSPECIFIED. ) ;
#3239=ORIENTED_EDGE ( 'NONE', *, *, #4906, .T. ) ;
#3256=DIRECTION ( 'NONE',  ( 1.000000000000000000, 3.286707217423839940E-17, 2.273843122241288053E-18 ) ) ;
#3268=CARTESIAN_POINT ( 'NONE',  ( 3.951447005078475350, 1.347150628109120563, -3.499999999999995559 ) ) ;
#3270=CARTESIAN_POINT ( 'NONE',  ( 4.158806965674308742, -1.986429158307094101, -3.559403772175848690 ) ) ;
#3274=EDGE_LOOP ( 'NONE', ( #4705, #5728, #11239 ) ) ;
#3279=CARTESIAN_POINT ( 'NONE',  ( 4.158921614371303477, 4.076055977742297110, -0.05993604794451207196 ) ) ;
#3293=CARTESIAN_POINT ( 'NONE',  ( 4.114405500665256454, 2.025575754679707963, -3.508400121684933204 ) ) ;
#3302=ORIENTED_EDGE ( 'NONE', *, *, #8010, .T. ) ;
#3306=AXIS2_PLACEMENT_3D ( 'NONE', #9096, #11438, #10137 ) ;
#3331=CARTESIAN_POINT ( 'NONE',  ( 4.175813232069169878, -2.061359961916378492, -3.570380186727409200 ) ) ;
#3334=B_SPLINE_CURVE_WITH_KNOTS ( 'NONE', 3,
 ( #11145, #31, #6827, #7702 ),
 .UNSPECIFIED., .F., .F.,
 ( 4, 4 ),
 ( 2.380739282295133395E-07, 0.002044882221487524538 ),
 .UNSPECIFIED. ) ;
#3338=CIRCLE ( 'NONE', #13390, 2.499999999999999112 ) ;
#3349=PLANE ( 'NONE',  #440 ) ;
#3351=CARTESIAN_POINT ( 'NONE',  ( 3.806834918298607651, -6.505213034913026604E-16, 3.499999999999989342 ) ) ;
#3358=CARTESIAN_POINT ( 'NONE',  ( 4.052424581287640493, 3.786734753434984668, 0.5771415817956560002 ) ) ;
#3365=CARTESIAN_POINT ( 'NONE',  ( 0.000000000000000000, 0.000000000000000000, 0.000000000000000000 ) ) ;
#3377=CARTESIAN_POINT ( 'NONE',  ( 4.093692494532781723, -2.021783646005765878, 3.501831996793828949 ) ) ;
#3391=AXIS2_PLACEMENT_3D ( 'NONE', #4664, #7870, #6912 ) ;
#3424=CARTESIAN_POINT ( 'NONE',  ( 3.878096787214409868, 3.381939201670029149, 1.142309474598562469 ) ) ;
#3429=CARTESIAN_POINT ( 'NONE',  ( 4.158807179406251109, 2.089320655794530079, -3.499999999999992450 ) ) ;
#3437=CARTESIAN_POINT ( 'NONE',  ( 5.599999999999994316, -2.020725942163681399, 3.499999999999989342 ) ) ;
#3439=CARTESIAN_POINT ( 'NONE',  ( 4.165266963751697915, -2.049631966911992453, 3.550066703508901966 ) ) ;
#3456=ORIENTED_EDGE ( 'NONE', *, *, #3809, .T. ) ;
#3461=ORIENTED_EDGE ( 'NONE', *, *, #11129, .T. ) ;
#3479=CONICAL_SURFACE ( 'NONE', #11642, 3.499999999999999112, 1.047197551196600296 ) ;
#3485=CARTESIAN_POINT ( 'NONE',  ( 4.151274195509662590, -2.039912954708747339, -3.533232880573491830 ) ) ;
#3495=CARTESIAN_POINT ( 'NONE',  ( 4.086376042167603195, 4.082715877136856797, -0.07147133206918650228 ) ) ;
#3505=CARTESIAN_POINT ( 'NONE',  ( 5.599999999999994316, 7.549649045036406812E-16, -2.499999999999999556 ) ) ;
#3517=ORIENTED_EDGE ( 'NONE', *, *, #6273, .T. ) ;
#3519=( NAMED_UNIT ( * ) SI_UNIT ( $, .STERADIAN. ) SOLID_ANGLE_UNIT ( ) );
#3536=FACE_OUTER_BOUND ( 'NONE', #9217, .T. ) ;
#3550=EDGE_CURVE ( 'NONE', #6673, #79, #3338, .T. ) ;
#3624=CARTESIAN_POINT ( 'NONE',  ( 4.158413352280787123, 2.044871626972824430, 3.541821552872956413 ) ) ;
#3630=CARTESIAN_POINT ( 'NONE',  ( 3.972709601346604114, 2.746729940827179028, -2.374099244652740914 ) ) ;
#3631=CARTESIAN_POINT ( 'NONE',  ( 5.599999999999994316, 2.020725942163681399, 3.499999999999996003 ) ) ;
#3641=EDGE_CURVE ( 'NONE', #4271, #8264, #2319, .T. ) ;
#3659=CARTESIAN_POINT ( 'NONE',  ( 4.175813232069169878, -2.061359961916364725, 3.570380186727409200 ) ) ;
#3660=ORIENTED_EDGE ( 'NONE', *, *, #11848, .F. ) ;
#3664=SURFACE_SIDE_STYLE ('',( #13695 ) ) ;
#3672=ORIENTED_EDGE ( 'NONE', *, *, #9342, .F. ) ;
#3721=CARTESIAN_POINT ( 'NONE',  ( 0.000000000000000000, 3.031088913245522320, 1.750000000000001554 ) ) ;
#3727=VERTEX_POINT ( 'NONE', #13293 ) ;
#3751=ORIENTED_EDGE ( 'NONE', *, *, #1371, .T. ) ;
#3760=CARTESIAN_POINT ( 'NONE',  ( 4.170895651974823259, 2.054890354522521001, 3.559174498016414834 ) ) ;
#3765=DIRECTION ( 'NONE',  ( -1.000000000000000000, -3.286707217423839940E-17, -2.273843122241288053E-18 ) ) ;
#3795=CARTESIAN_POINT ( 'NONE',  ( 3.961557105775776133, -1.423285172353590422, 3.499999999999993339 ) ) ;
#3798=ORIENTED_EDGE ( 'NONE', *, *, #10446, .F. ) ;
#3809=EDGE_CURVE ( 'NONE', #5579, #12256, #9706, .T. ) ;
#3815=DIRECTION ( 'NONE',  ( 0.000000000000000000, -5.551115123125782702E-17, -1.000000000000000000 ) ) ;
#3832=DIRECTION ( 'NONE',  ( -2.273843122241270334E-18, -5.551115123125782702E-17, -1.000000000000000000 ) ) ;
#3833=CARTESIAN_POINT ( 'NONE',  ( 4.175813232069169878, 2.061359961916364725, 3.570380186727388327 ) ) ;
#3836=PRODUCT_DEFINITION_FORMATION_WITH_SPECIFIED_SOURCE ( 'ANY', '', #10587, .NOT_KNOWN. ) ;
#3846=ORIENTED_EDGE ( 'NONE', *, *, #6197, .T. ) ;
#3847=CARTESIAN_POINT ( 'NONE',  ( 4.142654963991842187, 4.070796997468695722, -7.041181996303254420E-15 ) ) ;
#3886=CARTESIAN_POINT ( 'NONE',  ( 0.2175679805369626907, -1.691499766289308537, 3.499999999999996447 ) ) ;
#3897=SHAPE_REPRESENTATION_RELATIONSHIP ( 'NONE' , 'NONE' ,  #2934, #2974 ) ;
#3899=ORIENTED_EDGE ( 'NONE', *, *, #6661, .F. ) ;
#3903=AXIS2_PLACEMENT_3D ( 'NONE', #1713, #9687, #6235 ) ;
#3935=ORIENTED_EDGE ( 'NONE', *, *, #10334, .T. ) ;
#3936=CARTESIAN_POINT ( 'NONE',  ( 4.151274195509659926, -4.079825909417491125, -1.361623441637700086E-14 ) ) ;
#3969=CARTESIAN_POINT ( 'NONE',  ( 0.3126073911696169993, 2.020725942163681399, 3.499999999999996003 ) ) ;
#3974=STYLED_ITEM ( 'NONE', ( #13477 ), #1997 ) ;
#3975=EDGE_CURVE ( 'NONE', #1103, #7272, #12644, .T. ) ;
#3989=LINE ( 'NONE', #766, #8413 ) ;
#4011=CARTESIAN_POINT ( 'NONE',  ( 4.055492966679334010, 3.795017426213870504, -0.5629142681435886919 ) ) ;
#4022=FACE_OUTER_BOUND ( 'NONE', #12111, .T. ) ;
#4055=CARTESIAN_POINT ( 'NONE',  ( 3.973110223767151616, 2.262797354954571809E-11, 3.565797985667430225 ) ) ;
#4092=VERTEX_POINT ( 'NONE', #10038 ) ;
#4107=CARTESIAN_POINT ( 'NONE',  ( 0.000000000000000000, 0.000000000000000000, 0.000000000000000000 ) ) ;
#4117=CARTESIAN_POINT ( 'NONE',  ( 5.599999999999994316, 3.543787447695206106E-16, -5.200000000000001066 ) ) ;
#4143=CARTESIAN_POINT ( 'NONE',  ( 4.158413352280787123, 4.089743253945648860, -1.387778780781445676E-14 ) ) ;
#4185=CARTESIAN_POINT ( 'NONE',  ( 4.630153689607063860, 0.000000000000000000, 0.000000000000000000 ) ) ;
#4189=ADVANCED_FACE ( 'NONE', ( #3536 ), #13565, .F. ) ;
#4214=AXIS2_PLACEMENT_3D ( 'NONE', #14132, #8251, #7076 ) ;
#4238=CARTESIAN_POINT ( 'NONE',  ( 3.974183935050564997, -0.7239581970533717215, 3.565826011443126831 ) ) ;
#4264=CARTESIAN_POINT ( 'NONE',  ( 4.158806965674310518, -4.075748668183996060, -0.05940377217585728065 ) ) ;
#4266=CARTESIAN_POINT ( 'NONE',  ( 4.158413352280787123, -2.044871626972824430, 3.541821552872963075 ) ) ;
#4271=VERTEX_POINT ( 'NONE', #452 ) ;
#4276=B_SPLINE_CURVE_WITH_KNOTS ( 'NONE', 3,
 ( #3833, #11797, #13926, #4055 ),
 .UNSPECIFIED., .F., .F.,
 ( 4, 4 ),
 ( 0.000000000000000000, 0.002080789711329273685 ),
 .UNSPECIFIED. ) ;
#4286=CARTESIAN_POINT ( 'NONE',  ( 30.15499999999998693, 7.549649045036407798E-16, -2.499999999999999556 ) ) ;
#4288=PRODUCT_DEFINITION_CONTEXT ( 'detailed design', #5115, 'design' ) ;
#4298=AXIS2_PLACEMENT_3D ( 'NONE', #6530, #13153, #10725 ) ;
#4315=CARTESIAN_POINT ( 'NONE',  ( 3.880214671983573727, -0.7309020039786382483, 3.499999999999992895 ) ) ;
#4325=EDGE_LOOP ( 'NONE', ( #4407, #1104, #13454 ) ) ;
#4332=DIRECTION ( 'NONE',  ( -0.7071067811865513475, 2.410276454430290041E-17, -0.7071067811865435759 ) ) ;
#4334=CARTESIAN_POINT ( 'NONE',  ( 4.158413352280787123, 2.044871626972824430, -3.541821552872970180 ) ) ;
#4340=ORIENTED_EDGE ( 'NONE', *, *, #11879, .T. ) ;
#4376=CARTESIAN_POINT ( 'NONE',  ( 3.958484000407149761, -3.734437307742073386, -0.5317648453100152217 ) ) ;
#4377=DIRECTION ( 'NONE',  ( 1.000000000000000000, 3.286707217423839940E-17, -2.273843122241290364E-18 ) ) ;
#4380=CARTESIAN_POINT ( 'NONE',  ( 4.055498735588713544, -1.410041617599688601, 3.568038744583310162 ) ) ;
#4390=ORIENTED_EDGE ( 'NONE', *, *, #5350, .F. ) ;
#4407=ORIENTED_EDGE ( 'NONE', *, *, #1816, .T. ) ;
#4442=CARTESIAN_POINT ( 'NONE',  ( 3.951447005078477126, -3.704664227300094925, -0.5833333333333349247 ) ) ;
#4451=CARTESIAN_POINT ( 'NONE',  ( 3.951447005078475350, -3.704664227300094037, 0.5833333333333315940 ) ) ;
#4452=CARTESIAN_POINT ( 'NONE',  ( 3.972066048304797370, 2.740530939476389261, -2.384802634787859255 ) ) ;
#4454=PLANE ( 'NONE',  #9059 ) ;
#4460=CARTESIAN_POINT ( 'NONE',  ( 4.180231891692613111, 2.049421325483194778, 3.591231015387271519 ) ) ;
#4486=VECTOR ( 'NONE', #12915, 1000.000000000000000 ) ;
#4510=DIRECTION ( 'NONE',  ( -2.273843122241288438E-18, -5.551115123125783935E-17, -1.000000000000000000 ) ) ;
#4542=CARTESIAN_POINT ( 'NONE',  ( 30.60000000000001563, 0.000000000000000000, 0.000000000000000000 ) ) ;
#4545=LINE ( 'NONE', #3437, #7980 ) ;
#4548=CARTESIAN_POINT ( 'NONE',  ( 4.180345304246193550, -2.049116244671343789, 3.591763845239304143 ) ) ;
#4549=CARTESIAN_POINT ( 'NONE',  ( 4.151274195509663478, -2.039912954708747339, 3.533232880573498047 ) ) ;
#4586=FACE_OUTER_BOUND ( 'NONE', #265, .T. ) ;
#4590=DIRECTION ( 'NONE',  ( -1.000000000000000000, -3.286707217423839940E-17, -2.273843122241288053E-18 ) ) ;
#4608=EDGE_CURVE ( 'NONE', #13561, #6548, #14104, .T. ) ;
#4610=CARTESIAN_POINT ( 'NONE',  ( 4.086376042167603195, -1.979461949354205164, 3.571471332069175997 ) ) ;
#4639=CARTESIAN_POINT ( 'NONE',  ( 4.175813232069169878, -2.061359961916378492, -3.570380186727409200 ) ) ;
#4647=CARTESIAN_POINT ( 'NONE',  ( 4.071447262713911996, -2.020725942163681399, 3.499999999999989342 ) ) ;
#4664=CARTESIAN_POINT ( 'NONE',  ( 5.099999999999993427, 0.000000000000000000, 0.000000000000000000 ) ) ;
#4684=EDGE_CURVE ( 'NONE', #2270, #4092, #10888, .T. ) ;
#4705=ORIENTED_EDGE ( 'NONE', *, *, #1873, .T. ) ;
#4745=CARTESIAN_POINT ( 'NONE',  ( 0.3126073911696169993, 4.041451884327390331, 0.000000000000000000 ) ) ;
#4750=ORIENTED_EDGE ( 'NONE', *, *, #12459, .F. ) ;
#4815=EDGE_LOOP ( 'NONE', ( #9474, #2568, #477, #646 ) ) ;
#4858=FACE_OUTER_BOUND ( 'NONE', #8203, .T. ) ;
#4889=ORIENTED_EDGE ( 'NONE', *, *, #12459, .T. ) ;
#4896=CARTESIAN_POINT ( 'NONE',  ( -2.696105871110437585E-15, -0.3420925509381240182, 3.499999999999996891 ) ) ;
#4906=EDGE_CURVE ( 'NONE', #2047, #2270, #7649, .T. ) ;
#4910=( NAMED_UNIT ( * ) PLANE_ANGLE_UNIT ( ) SI_UNIT ( $, .RADIAN. ) );
#4917=ORIENTED_EDGE ( 'NONE', *, *, #4684, .F. ) ;
#4919=CIRCLE ( 'NONE', #7474, 3.499999999999999112 ) ;
#4930=ADVANCED_FACE ( 'NONE', ( #2240, #14393 ), #1133, .T. ) ;
#4972=FACE_OUTER_BOUND ( 'NONE', #5039, .T. ) ;
#4999=EDGE_LOOP ( 'NONE', ( #11377, #3935, #5398, #1946 ) ) ;
#5006=COLOUR_RGB ( '', 0.31764706, 0.68627451, 0.89019608) ;
#5039=EDGE_LOOP ( 'NONE', ( #12919, #12389, #8672, #10239, #10737 ) ) ;
#5042=ADVANCED_FACE ( 'NONE', ( #12399 ), #2710, .T. ) ;
#5051=CARTESIAN_POINT ( 'NONE',  ( 5.599999999999994316, 0.000000000000000000, 0.000000000000000000 ) ) ;
#5075=LINE ( 'NONE', #11744, #6794 ) ;
#5094=CARTESIAN_POINT ( 'NONE',  ( 4.175813232069169878, -2.061359961916364725, 3.570380186727409200 ) ) ;
#5109=CARTESIAN_POINT ( 'NONE',  ( 0.000000000000000000, 1.387778780781445676E-14, 3.499999999999982236 ) ) ;
#5111=DIRECTION ( 'NONE',  ( 2.960064101202773706E-17, 0.8660254037844384856, 0.5000000000000004441 ) ) ;
#5115=APPLICATION_CONTEXT ( 'automotive_design' ) ;
#5130=ORIENTED_EDGE ( 'NONE', *, *, #11187, .T. ) ;
#5173=CARTESIAN_POINT ( 'NONE',  ( 3.973110223765541793, 0.6902454861566493793, -3.565797985667388481 ) ) ;
#5257=ORIENTED_EDGE ( 'NONE', *, *, #10196, .F. ) ;
#5263=DIRECTION ( 'NONE',  ( -1.000000000000000000, -3.286707217423839940E-17, -2.273843122241288053E-18 ) ) ;
#5274=CARTESIAN_POINT ( 'NONE',  ( 5.599999999999994316, 7.263589608730915515E-16, 2.499999999999999556 ) ) ;
#5313=ORIENTED_EDGE ( 'NONE', *, *, #11467, .F. ) ;
#5322=ORIENTED_EDGE ( 'NONE', *, *, #13571, .T. ) ;
#5335=CARTESIAN_POINT ( 'NONE',  ( 4.175075985190068728, -2.060370777630105010, 3.568666869285572307 ) ) ;
#5342=CARTESIAN_POINT ( 'NONE',  ( -6.209175019847646269E-15, 2.859595677584334528, -2.047034997319569616 ) ) ;
#5350=EDGE_CURVE ( 'NONE', #1315, #269, #10758, .T. ) ;
#5388=AXIS2_PLACEMENT_3D ( 'NONE', #12247, #7839, #12315 ) ;
#5396=CARTESIAN_POINT ( 'NONE',  ( 3.961545574369877531, 1.423222908132143250, -3.499999999999992450 ) ) ;
#5398=ORIENTED_EDGE ( 'NONE', *, *, #2893, .F. ) ;
#5406=CARTESIAN_POINT ( 'NONE',  ( 4.175326769692829565, 2.060699556488938100, -3.569236330973477589 ) ) ;
#5407=ORIENTED_EDGE ( 'NONE', *, *, #4684, .T. ) ;
#5409=ORIENTED_EDGE ( 'NONE', *, *, #350, .T. ) ;
#5441=DIRECTION ( 'NONE',  ( 1.000000000000000000, 0.000000000000000000, 0.000000000000000000 ) ) ;
#5463=B_SPLINE_CURVE_WITH_KNOTS ( 'NONE', 3,
 ( #5989, #2357, #10399, #13644 ),
 .UNSPECIFIED., .F., .F.,
 ( 4, 4 ),
 ( 0.000000000000000000, 0.002080789711329283660 ),
 .UNSPECIFIED. ) ;
#5469=CARTESIAN_POINT ( 'NONE',  ( 4.180232103119972287, 2.085387772176683807, -3.570466442734691270 ) ) ;
#5474=FACE_OUTER_BOUND ( 'NONE', #2784, .T. ) ;
#5479=CARTESIAN_POINT ( 'NONE',  ( 5.599999999999994316, 2.886579864025407597E-16, 5.200000000000001066 ) ) ;
#5504=CARTESIAN_POINT ( 'NONE',  ( 4.050823680195247078, -3.779313952391379683, 0.5899027668435089522 ) ) ;
#5527=CARTESIAN_POINT ( 'NONE',  ( 3.961551342853779190, 2.319461885623249398, 2.982574167880994498 ) ) ;
#5537=CARTESIAN_POINT ( 'NONE',  ( 3.972709601346610331, 3.429395227388317924, 1.191688283765310219 ) ) ;
#5539=CARTESIAN_POINT ( 'NONE',  ( 4.165266963751699691, 2.049631966911994230, -3.550066703508909960 ) ) ;
#5561=AXIS2_PLACEMENT_3D ( 'NONE', #5734, #6777, #12493 ) ;
#5579=VERTEX_POINT ( 'NONE', #9035 ) ;
#5583=ADVANCED_FACE ( 'NONE', ( #12348 ), #2354, .F. ) ;
#5584=CARTESIAN_POINT ( 'NONE',  ( 4.180231891692621993, -2.049421325483208989, -3.591231015387289727 ) ) ;
#5591=DIRECTION ( 'NONE',  ( 0.000000000000000000, 5.551115123125782702E-17, 1.000000000000000000 ) ) ;
#5602=CARTESIAN_POINT ( 'NONE',  ( 3.974167765203679537, 0.7238254970443265268, -3.565825589389254979 ) ) ;
#5603=ADVANCED_FACE ( 'NONE', ( #11098 ), #8899, .T. ) ;
#5605=DIRECTION ( 'NONE',  ( -1.000000000000000000, -3.286707217423839940E-17, -2.273843122241288053E-18 ) ) ;
#5622=FILL_AREA_STYLE ('',( #10095 ) ) ;
#5647=CIRCLE ( 'NONE', #7759, 3.499999999999999112 ) ;
#5655=DIRECTION ( 'NONE',  ( 1.840274199520074535E-17, 0.5000000000000019984, 0.8660254037844375974 ) ) ;
#5660=LINE ( 'NONE', #3631, #8891 ) ;
#5672=CARTESIAN_POINT ( 'NONE',  ( 3.958476099524994130, -1.406653531809710644, -3.499999999999992895 ) ) ;
#5675=CARTESIAN_POINT ( 'NONE',  ( 0.3126073911696169993, 4.041451884327390331, 0.000000000000000000 ) ) ;
#5680=CARTESIAN_POINT ( 'NONE',  ( 4.158921614371304365, -1.986121848748764851, 3.559936047944501247 ) ) ;
#5715=CARTESIAN_POINT ( 'NONE',  ( 5.599999999999994316, 4.041451884327390331, 0.000000000000000000 ) ) ;
#5717=EDGE_CURVE ( 'NONE', #11894, #1315, #13167, .T. ) ;
#5728=ORIENTED_EDGE ( 'NONE', *, *, #5717, .T. ) ;
#5734=CARTESIAN_POINT ( 'NONE',  ( 5.599999999999994316, 2.020725942163681399, -3.499999999999996003 ) ) ;
#5748=CARTESIAN_POINT ( 'NONE',  ( 0.1388410611046012044, -2.351840044243032057, 2.926493552096011364 ) ) ;
#5755=DIRECTION ( 'NONE',  ( -1.000000000000000000, -3.286707217423839940E-17, -2.273843122241288053E-18 ) ) ;
#5782=CARTESIAN_POINT ( 'NONE',  ( 4.114405500665253790, 2.025575754679707075, 3.508400121684931428 ) ) ;
#5851=EDGE_CURVE ( 'NONE', #14160, #4271, #6842, .T. ) ;
#5859=CARTESIAN_POINT ( 'NONE',  ( 0.000000000000000000, 0.000000000000000000, 0.000000000000000000 ) ) ;
#5872=EDGE_LOOP ( 'NONE', ( #541, #6769, #14123 ) ) ;
#5906=CARTESIAN_POINT ( 'NONE',  ( 0.3126073911696169993, 2.020725942163681399, 3.499999999999996003 ) ) ;
#5909=ADVANCED_FACE ( 'NONE', ( #6106 ), #10860, .F. ) ;
#5934=CARTESIAN_POINT ( 'NONE',  ( 4.082498951862934433, -2.020725942163681399, -3.500000000000010214 ) ) ;
#5966=ADVANCED_FACE ( 'NONE', ( #4586 ), #11407, .F. ) ;
#5972=CARTESIAN_POINT ( 'NONE',  ( 0.02993401039713041584, -2.688325911136451030, 2.343682934607755897 ) ) ;
#5989=CARTESIAN_POINT ( 'NONE',  ( 4.175813232069169878, -2.061359961916378492, -3.570380186727409200 ) ) ;
#6035=EDGE_CURVE ( 'NONE', #7658, #11064, #9271, .T. ) ;
#6064=CARTESIAN_POINT ( 'NONE',  ( 0.1397371499203141909, 1.362866705341260865, 3.499999999999996447 ) ) ;
#6077=PLANE ( 'NONE',  #3903 ) ;
#6097=COLOUR_RGB ( '', 0.31764706, 0.68627451, 0.89019608) ;
#6106=FACE_OUTER_BOUND ( 'NONE', #797, .T. ) ;
#6149=SURFACE_STYLE_FILL_AREA ( #2728 ) ;
#6153=EDGE_CURVE ( 'NONE', #13171, #2841, #1959, .T. ) ;
#6166=ORIENTED_EDGE ( 'NONE', *, *, #1624, .F. ) ;
#6191=CARTESIAN_POINT ( 'NONE',  ( 3.961551342854645608, 3.742715940867690882, -0.5174258321192194421 ) ) ;
#6197=EDGE_CURVE ( 'NONE', #6262, #10783, #3989, .T. ) ;
#6215=CARTESIAN_POINT ( 'NONE',  ( 4.055492966679429045, -3.795017426214134293, 0.5629142681437507845 ) ) ;
#6223=SURFACE_SIDE_STYLE ('',( #6149 ) ) ;
#6235=DIRECTION ( 'NONE',  ( 2.273843122241288438E-18, 5.551115123125783935E-17, 1.000000000000000000 ) ) ;
#6257=CARTESIAN_POINT ( 'NONE',  ( 3.950241966888154099, 3.393956070637165201, -1.121495646999262075 ) ) ;
#6262=VERTEX_POINT ( 'NONE', #12033 ) ;
#6270=EDGE_CURVE ( 'NONE', #172, #14160, #2653, .T. ) ;
#6273=EDGE_CURVE ( 'NONE', #2047, #10405, #9827, .T. ) ;
#6324=PLANE ( 'NONE',  #10205 ) ;
#6333=CARTESIAN_POINT ( 'NONE',  ( 4.170895651974873886, -4.109780709045213420, -7.786222839923386950E-14 ) ) ;
#6362=EDGE_LOOP ( 'NONE', ( #2102, #14111, #9532, #8530 ) ) ;
#6385=CARTESIAN_POINT ( 'NONE',  ( 4.170895651974874774, 4.109780709045202762, 1.691345105195479668E-14 ) ) ;
#6393=TOROIDAL_SURFACE ( 'NONE', #3391, 5.200000000000001066, 0.4999999999999975020 ) ;
#6395=CARTESIAN_POINT ( 'NONE',  ( 30.60000000000001563, 0.000000000000000000, 0.000000000000000000 ) ) ;
#6426=CARTESIAN_POINT ( 'NONE',  ( 4.071447262713911996, -2.020725942163681399, 3.499999999999989342 ) ) ;
#6444=CARTESIAN_POINT ( 'NONE',  ( 3.972709601346603225, -2.746729940827184802, 2.374099244652728924 ) ) ;
#6462=CARTESIAN_POINT ( 'NONE',  ( 4.052424581288006422, -3.786734753435994083, -0.5771415817964102857 ) ) ;
#6473=CIRCLE ( 'NONE', #2512, 5.371010071662830399 ) ;
#6487=AXIS2_PLACEMENT_3D ( 'NONE', #13798, #7185, #2516 ) ;
#6524=DIRECTION ( 'NONE',  ( 0.000000000000000000, 0.000000000000000000, 1.000000000000000000 ) ) ;
#6530=CARTESIAN_POINT ( 'NONE',  ( 0.000000000000000000, 0.000000000000000000, 0.000000000000000000 ) ) ;
#6534=CARTESIAN_POINT ( 'NONE',  ( 3.951447005078477126, -2.357513599190964371, 2.916666666666658081 ) ) ;
#6548=VERTEX_POINT ( 'NONE', #4117 ) ;
#6562=CARTESIAN_POINT ( 'NONE',  ( 4.050536630291714069, 3.778525289263168219, 0.5912575323401301208 ) ) ;
#6565=CARTESIAN_POINT ( 'NONE',  ( 4.175572532730952524, 2.061029303918050282, -3.569807470274386496 ) ) ;
#6569=VECTOR ( 'NONE', #13181, 1000.000000000000000 ) ;
#6577=DIRECTION ( 'NONE',  ( 0.000000000000000000, 5.551115123125782702E-17, 1.000000000000000000 ) ) ;
#6598=EDGE_CURVE ( 'NONE', #9365, #6262, #1615, .T. ) ;
#6603=CARTESIAN_POINT ( 'NONE',  ( 4.071447262713911996, -4.041451884327377009, 0.000000000000000000 ) ) ;
#6628=CARTESIAN_POINT ( 'NONE',  ( 0.1381419387119249831, -1.355287006778807868, -3.499999999999996003 ) ) ;
#6630=CARTESIAN_POINT ( 'NONE',  ( 4.055487192203054647, 1.409979666029696155, -3.568038521265871399 ) ) ;
#6636=VERTEX_POINT ( 'NONE', #5675 ) ;
#6639=DIRECTION ( 'NONE',  ( 0.000000000000000000, -5.551115123125782702E-17, -1.000000000000000000 ) ) ;
#6645=EDGE_CURVE ( 'NONE', #6262, #9365, #13556, .T. ) ;
#6661=EDGE_CURVE ( 'NONE', #14126, #11894, #12132, .T. ) ;
#6673=VERTEX_POINT ( 'NONE', #3505 ) ;
#6686=CARTESIAN_POINT ( 'NONE',  ( 4.086376042167605860, 1.979461949354207828, -3.571471332069182658 ) ) ;
#6711=CARTESIAN_POINT ( 'NONE',  ( 4.630153689607063860, 9.559099815976924059E-16, 5.371010071662830399 ) ) ;
#6729=ORIENTED_EDGE ( 'NONE', *, *, #1371, .F. ) ;
#6736=CONICAL_SURFACE ( 'NONE', #9303, 3.499999999999999112, 1.047197551196600296 ) ;
#6745=CARTESIAN_POINT ( 'NONE',  ( 4.050536630291718510, -3.778525289263177989, -0.5912575323401209060 ) ) ;
#6753=CARTESIAN_POINT ( 'NONE',  ( 4.030867648404682591, -3.732851566702919843, -0.5345114293595707444 ) ) ;
#6765=CARTESIAN_POINT ( 'NONE',  ( 4.158806965674299860, 1.986429158307079224, 3.559403772175830927 ) ) ;
#6769=ORIENTED_EDGE ( 'NONE', *, *, #8768, .T. ) ;
#6777=DIRECTION ( 'NONE',  ( 2.273843122241273031E-18, -2.220446049250313574E-16, 1.000000000000000000 ) ) ;
#6794=VECTOR ( 'NONE', #7268, 1000.000000000000114 ) ;
#6796=( NAMED_UNIT ( * ) PLANE_ANGLE_UNIT ( ) SI_UNIT ( $, .RADIAN. ) );
#6827=CARTESIAN_POINT ( 'NONE',  ( -5.736770013510187597E-15, -3.375361811986495653, 1.153701847711628536 ) ) ;
#6835=CARTESIAN_POINT ( 'NONE',  ( 0.000000000000000000, 0.000000000000000000, 0.000000000000000000 ) ) ;
#6842=B_SPLINE_CURVE_WITH_KNOTS ( 'NONE', 3,
 ( #2991, #7489, #7285, #7360, #6333, #11835, #11677, #3936, #8534, #8597, #786, #8673, #14115, #13084, #7207, #9491 ),
 .UNSPECIFIED., .F., .F.,
 ( 4, 3, 3, 3, 3, 4 ),
 ( -2.111273352586108592E-06, 0.000000000000000000, 3.519286887797300651E-05, 7.191842652071138019E-05, 0.0001049868727093777871, 0.0001382836236822087195 ),
 .UNSPECIFIED. ) ;
#6845=CARTESIAN_POINT ( 'NONE',  ( 3.958484000407669345, 3.734437307742072942, 0.5317648453099808048 ) ) ;
#6855=B_SPLINE_CURVE_WITH_KNOTS ( 'NONE', 3,
 ( #5906, #6937, #368, #12574 ),
 .UNSPECIFIED., .F., .F.,
 ( 4, 4 ),
 ( 2.380739282218358329E-07, 0.002044882221487521069 ),
 .UNSPECIFIED. ) ;
#6885=( NAMED_UNIT ( * ) PLANE_ANGLE_UNIT ( ) SI_UNIT ( $, .RADIAN. ) );
#6897=CARTESIAN_POINT ( 'NONE',  ( 4.165266963751700580, -2.049631966911993786, -3.550066703508896637 ) ) ;
#6898=CARTESIAN_POINT ( 'NONE',  ( 0.000000000000000000, 0.000000000000000000, 0.000000000000000000 ) ) ;
#6900=CARTESIAN_POINT ( 'NONE',  ( 3.951447005078475350, -1.347150628109120785, 3.499999999999988454 ) ) ;
#6912=DIRECTION ( 'NONE',  ( -2.273843122241289979E-18, 5.551115123125782702E-17, 1.000000000000000000 ) ) ;
#6930=CARTESIAN_POINT ( 'NONE',  ( 0.000000000000000000, 0.000000000000000000, 0.000000000000000000 ) ) ;
#6932=CARTESIAN_POINT ( 'NONE',  ( -7.055360934154693097E-15, -2.859595677584332307, 2.047034997319569172 ) ) ;
#6937=CARTESIAN_POINT ( 'NONE',  ( 0.1217565302851122550, 2.351289329882154888, 2.927447417349537950 ) ) ;
#6969=ORIENTED_EDGE ( 'NONE', *, *, #1730, .T. ) ;
#6972=EDGE_LOOP ( 'NONE', ( #11494, #10908 ) ) ;
#6983=CARTESIAN_POINT ( 'NONE',  ( 0.03027795055833474094, 0.6888063905328563052, -3.499999999999995559 ) ) ;
#6985=B_SPLINE_CURVE_WITH_KNOTS ( 'NONE', 3,
 ( #10736, #5173, #7133, #419 ),
 .UNSPECIFIED., .F., .F.,
 ( 4, 4 ),
 ( 0.002080789711329283660, 0.004173039763574516899 ),
 .UNSPECIFIED. ) ;
#6996=ORIENTED_EDGE ( 'NONE', *, *, #9342, .T. ) ;
#7016=EDGE_CURVE ( 'NONE', #6548, #13561, #2785, .T. ) ;
#7031=CONICAL_SURFACE ( 'NONE', #750, 5.371010071662830399, 1.221730476396037268 ) ;
#7034=CARTESIAN_POINT ( 'NONE',  ( 4.151274195509659037, 2.039912954708745119, 3.533232880573488721 ) ) ;
#7064=CARTESIAN_POINT ( 'NONE',  ( 0.1217565302851075920, 3.710888496608915510, -0.5725525826504623828 ) ) ;
#7076=DIRECTION ( 'NONE',  ( -1.840274199520073302E-17, -0.5000000000000013323, -0.8660254037844379305 ) ) ;
#7080=CARTESIAN_POINT ( 'NONE',  ( 0.000000000000000000, 1.387778780781445676E-14, 3.499999999999982236 ) ) ;
#7123=DIRECTION ( 'NONE',  ( 0.000000000000000000, -6.695352868347746904E-17, 1.000000000000000000 ) ) ;
#7129=ORIENTED_EDGE ( 'NONE', *, *, #796, .F. ) ;
#7133=CARTESIAN_POINT ( 'NONE',  ( 4.050480423730761004, 1.376911654797406737, -3.567926555162020730 ) ) ;
#7176=CARTESIAN_POINT ( 'NONE',  ( 4.124214193018063135, 2.028338413290930120, 3.513185186763549073 ) ) ;
#7185=DIRECTION ( 'NONE',  ( -1.000000000000000000, -3.286707217423839940E-17, -2.273843122241288053E-18 ) ) ;
#7207=CARTESIAN_POINT ( 'NONE',  ( 4.082498951862936210, -4.041451884327377009, 2.512980736065759382E-20 ) ) ;
#7255=FACE_OUTER_BOUND ( 'NONE', #6972, .T. ) ;
#7259=CARTESIAN_POINT ( 'NONE',  ( 4.165266963751704132, 4.099263933823992012, -1.430665712853978865E-14 ) ) ;
#7268=DIRECTION ( 'NONE',  ( 0.3420201433256625512, -4.092221844761578132E-17, -0.9396926207859105373 ) ) ;
#7272=VERTEX_POINT ( 'NONE', #11966 ) ;
#7285=CARTESIAN_POINT ( 'NONE',  ( 4.175326769692884632, -4.121399112977863766, 1.938140992669738524E-14 ) ) ;
#7289=VECTOR ( 'NONE', #9830, 1000.000000000000000 ) ;
#7296=FACE_OUTER_BOUND ( 'NONE', #2648, .T. ) ;
#7308=CARTESIAN_POINT ( 'NONE',  ( 5.099999999999993427, 2.886579864025407597E-16, 5.200000000000001066 ) ) ;
#7309=VERTEX_POINT ( 'NONE', #10720 ) ;
#7324=CARTESIAN_POINT ( 'NONE',  ( 0.2182387239031207404, 1.693823289467343063, 3.499999999999995559 ) ) ;
#7332=UNCERTAINTY_MEASURE_WITH_UNIT (LENGTH_MEASURE( 1.000000000000000082E-05 ), #2288, 'distance_accuracy_value', 'NONE');
#7334=CARTESIAN_POINT ( 'NONE',  ( 0.1388410611046067000, -3.710337782248029015, -0.5735064479039794216 ) ) ;
#7343=ORIENTED_EDGE ( 'NONE', *, *, #3550, .T. ) ;
#7350=CARTESIAN_POINT ( 'NONE',  ( 5.599999999999994316, 4.041451884327390331, 0.000000000000000000 ) ) ;
#7360=CARTESIAN_POINT ( 'NONE',  ( 4.175075985190124683, -4.120741555260251765, 1.387778780781445676E-14 ) ) ;
#7364=CARTESIAN_POINT ( 'NONE',  ( 3.973110223767151616, 2.262797354954571809E-11, 3.565797985667430225 ) ) ;
#7406=AXIS2_PLACEMENT_3D ( 'NONE', #6395, #9760, #13151 ) ;
#7424=CARTESIAN_POINT ( 'NONE',  ( 4.033906725095162571, -1.419670120618688136, 3.499999999999992895 ) ) ;
#7435=EDGE_LOOP ( 'NONE', ( #3302, #14235, #5409 ) ) ;
#7441=EDGE_CURVE ( 'NONE', #11064, #4271, #9097, .T. ) ;
#7442=CARTESIAN_POINT ( 'NONE',  ( 0.000000000000000000, -3.031088913245536087, 1.750000000000001554 ) ) ;
#7446=SHAPE_DEFINITION_REPRESENTATION ( #415, #2934 ) ;
#7447=CARTESIAN_POINT ( 'NONE',  ( 4.630153689607063860, 0.000000000000000000, 0.000000000000000000 ) ) ;
#7474=AXIS2_PLACEMENT_3D ( 'NONE', #2534, #2604, #8374 ) ;
#7477=FACE_OUTER_BOUND ( 'NONE', #10656, .T. ) ;
#7485=CARTESIAN_POINT ( 'NONE',  ( 4.630153689607063860, 9.559099815976924059E-16, 5.371010071662830399 ) ) ;
#7489=CARTESIAN_POINT ( 'NONE',  ( 4.175572532730952524, -4.122058607836128097, 1.176423331927875400E-14 ) ) ;
#7495=CARTESIAN_POINT ( 'NONE',  ( 4.630153689607063860, 0.000000000000000000, 0.000000000000000000 ) ) ;
#7498=FACE_OUTER_BOUND ( 'NONE', #12663, .T. ) ;
#7503=CARTESIAN_POINT ( 'NONE',  ( 0.000000000000000000, 0.000000000000000000, -3.500000000000010214 ) ) ;
#7518=FACE_OUTER_BOUND ( 'NONE', #6362, .T. ) ;
#7564=CARTESIAN_POINT ( 'NONE',  ( 4.158921614371306141, 1.986121848748767071, -3.559936047944508797 ) ) ;
#7567=ADVANCED_FACE ( 'NONE', ( #8942 ), #14445, .T. ) ;
#7584=CARTESIAN_POINT ( 'NONE',  ( 5.684607805603219362E-18, 1.387778780781445182E-16, 2.499999999999999112 ) ) ;
#7587=CARTESIAN_POINT ( 'NONE',  ( 4.086262629614033415, -4.082406995609999534, -0.07093633357112584525 ) ) ;
#7601=CARTESIAN_POINT ( 'NONE',  ( -4.106788408769115985E-15, -2.686816014504578298, -2.346298152288348149 ) ) ;
#7628=CARTESIAN_POINT ( 'NONE',  ( 4.086262629614031638, -1.979770830881089738, -3.570936333571117505 ) ) ;
#7637=CARTESIAN_POINT ( 'NONE',  ( 4.030867648405330073, 3.732851566702002799, 0.5345114293581457732 ) ) ;
#7649=CIRCLE ( 'NONE', #7888, 3.499999999999999112 ) ;
#7658=VERTEX_POINT ( 'NONE', #4639 ) ;
#7686=AXIS2_PLACEMENT_3D ( 'NONE', #12067, #5263, #13179 ) ;
#7702=CARTESIAN_POINT ( 'NONE',  ( 0.000000000000000000, -3.031088913245536087, 1.750000000000001554 ) ) ;
#7707=CARTESIAN_POINT ( 'NONE',  ( 4.071447262713911996, -2.020725942163681399, -3.500000000000010214 ) ) ;
#7710=CARTESIAN_POINT ( 'NONE',  ( 4.180345304246198879, -4.135116856707401922, 0.02129519942689507561 ) ) ;
#7736=CARTESIAN_POINT ( 'NONE',  ( 3.958484000408148518, -2.327740518749091159, 2.968235154689833344 ) ) ;
#7759=AXIS2_PLACEMENT_3D ( 'NONE', #2959, #3107, #9531 ) ;
#7764=CARTESIAN_POINT ( 'NONE',  ( 0.3126073911695614882, -2.020725942163792421, -3.500000000000003109 ) ) ;
#7770=AXIS2_PLACEMENT_3D ( 'NONE', #13694, #8033, #10385 ) ;
#7774=CARTESIAN_POINT ( 'NONE',  ( 4.050823680195248855, -2.400527758044911142, -2.978030508226159778 ) ) ;
#7787=CARTESIAN_POINT ( 'NONE',  ( 5.599999999999994316, -4.041451884327377009, 0.000000000000000000 ) ) ;
#7788=CARTESIAN_POINT ( 'NONE',  ( 4.050536630291712292, 2.401306687817035268, -2.976670123173770222 ) ) ;
#7810=CARTESIAN_POINT ( 'NONE',  ( 3.973514160553479613, 2.741076955031366058, 2.383932505289871884 ) ) ;
#7813=CARTESIAN_POINT ( 'NONE',  ( 4.030867648405613402, -2.329326259788630171, 2.965488570640940846 ) ) ;
#7819=ORIENTED_EDGE ( 'NONE', *, *, #799, .T. ) ;
#7824=FACE_OUTER_BOUND ( 'NONE', #4999, .T. ) ;
#7830=ORIENTED_EDGE ( 'NONE', *, *, #1624, .T. ) ;
#7839=DIRECTION ( 'NONE',  ( -1.000000000000000000, -3.286707217423839940E-17, -2.273843122241288053E-18 ) ) ;
#7844=ORIENTED_EDGE ( 'NONE', *, *, #6661, .T. ) ;
#7862=CARTESIAN_POINT ( 'NONE',  ( 3.972066048304764507, 3.435565134476452620, 1.180968096049827443 ) ) ;
#7870=DIRECTION ( 'NONE',  ( -1.000000000000000000, -3.286707217423839940E-17, -2.273843122241288053E-18 ) ) ;
#7872=CARTESIAN_POINT ( 'NONE',  ( 4.030859730899669202, -1.403482646610284323, -3.499999999999992006 ) ) ;
#7888=AXIS2_PLACEMENT_3D ( 'NONE', #6898, #11152, #9018 ) ;
#7893=( LENGTH_UNIT ( ) NAMED_UNIT ( * ) SI_UNIT ( .MILLI., .METRE. ) );
#7895=B_SPLINE_CURVE_WITH_KNOTS ( 'NONE', 3,
 ( #13511, #10193, #12533, #8956, #10133 ),
 .UNSPECIFIED., .F., .F.,
 ( 4, 1, 4 ),
 ( 0.000000000000000000, 0.002020725942163691807, 0.004041451884327383615 ),
 .UNSPECIFIED. ) ;
#7937=ORIENTED_EDGE ( 'NONE', *, *, #10928, .T. ) ;
#7949=CARTESIAN_POINT ( 'NONE',  ( 4.071447262713911996, 2.020725942163681399, 3.499999999999996003 ) ) ;
#7980=VECTOR ( 'NONE', #1083, 1000.000000000000000 ) ;
#8010=EDGE_CURVE ( 'NONE', #10506, #1103, #2150, .T. ) ;
#8012=CARTESIAN_POINT ( 'NONE',  ( 0.1397371499203132750, 1.362866705341256868, -3.499999999999996891 ) ) ;
#8033=DIRECTION ( 'NONE',  ( -1.000000000000000000, -3.286707217423839940E-17, -2.273843122241288053E-18 ) ) ;
#8060=CARTESIAN_POINT ( 'NONE',  ( 4.175075985190068728, -2.060370777630091244, -3.568666869285586074 ) ) ;
#8072=B_SPLINE_CURVE_WITH_KNOTS ( 'NONE', 3,
 ( #11037, #6565, #5406, #9876, #14346, #5539, #4334, #2116, #9942, #8837, #13317, #3293, #2775, #13689, #1521, #204 ),
 .UNSPECIFIED., .F., .F.,
 ( 4, 3, 3, 3, 3, 4 ),
 ( -2.111273352583301948E-06, 0.000000000000000000, 3.519286887794339423E-05, 7.191842652067419205E-05, 0.0001049868727093471041, 0.0001382836236821663543 ),
 .UNSPECIFIED. ) ;
#8148=ORIENTED_EDGE ( 'NONE', *, *, #11559, .F. ) ;
#8156=VECTOR ( 'NONE', #10152, 1000.000000000000000 ) ;
#8178=CARTESIAN_POINT ( 'NONE',  ( 30.15499999999998693, 1.387778780781445182E-16, 2.499999999999999112 ) ) ;
#8198=STYLED_ITEM ( 'NONE', ( #2654 ), #2974 ) ;
#8203=EDGE_LOOP ( 'NONE', ( #3461, #3239, #5407 ) ) ;
#8214=VERTEX_POINT ( 'NONE', #8608 ) ;
#8231=ADVANCED_FACE ( 'NONE', ( #7498 ), #3479, .T. ) ;
#8239=CARTESIAN_POINT ( 'NONE',  ( 0.000000000000000000, 3.031088913245536087, -1.750000000000001554 ) ) ;
#8248=DIRECTION ( 'NONE',  ( -2.273843122241288438E-18, -5.551115123125783935E-17, -1.000000000000000000 ) ) ;
#8251=DIRECTION ( 'NONE',  ( -2.732679788978644593E-17, -0.8660254037844379305, 0.5000000000000013323 ) ) ;
#8264=VERTEX_POINT ( 'NONE', #11913 ) ;
#8276=ADVANCED_FACE ( 'NONE', ( #4022 ), #1806, .F. ) ;
#8278=CARTESIAN_POINT ( 'NONE',  ( 4.071447262713911996, 2.020725942163681399, 3.499999999999996003 ) ) ;
#8303=CARTESIAN_POINT ( 'NONE',  ( 30.60000000000001563, 1.451737380178518264E-16, -2.055000000000000160 ) ) ;
#8330=ORIENTED_EDGE ( 'NONE', *, *, #5851, .T. ) ;
#8342=AXIS2_PLACEMENT_3D ( 'NONE', #11770, #9572, #14051 ) ;
#8372=AXIS2_PLACEMENT_3D ( 'NONE', #1212, #9996, #5591 ) ;
#8374=DIRECTION ( 'NONE',  ( -2.273843122241288438E-18, -5.551115123125783935E-17, -1.000000000000000000 ) ) ;
#8391=AXIS2_PLACEMENT_3D ( 'NONE', #4542, #5605, #11247 ) ;
#8413=VECTOR ( 'NONE', #13872, 1000.000000000000114 ) ;
#8421=VECTOR ( 'NONE', #4332, 1000.000000000000114 ) ;
#8433=CIRCLE ( 'NONE', #2141, 0.4999999999999978351 ) ;
#8458=CARTESIAN_POINT ( 'NONE',  ( 3.880206590543185285, 3.396506438958528218, -1.117078279489001735 ) ) ;
#8464=CARTESIAN_POINT ( 'NONE',  ( 4.086262418390194995, -2.102635014057366636, 3.499999999999993339 ) ) ;
#8479=ORIENTED_EDGE ( 'NONE', *, *, #11129, .F. ) ;
#8522=ADVANCED_FACE ( 'NONE', ( #1870 ), #6324, .F. ) ;
#8524=ORIENTED_EDGE ( 'NONE', *, *, #11879, .F. ) ;
#8530=ORIENTED_EDGE ( 'NONE', *, *, #6270, .F. ) ;
#8534=CARTESIAN_POINT ( 'NONE',  ( 4.142654963991842187, -4.070796997468695722, -6.939432481254059658E-15 ) ) ;
#8546=CARTESIAN_POINT ( 'NONE',  ( 5.099999999999993427, 0.000000000000000000, 0.000000000000000000 ) ) ;
#8565=CARTESIAN_POINT ( 'NONE',  ( 0.000000000000000000, 1.387778780781445676E-14, 3.499999999999982236 ) ) ;
#8583=ADVANCED_FACE ( 'NONE', ( #7477 ), #11624, .T. ) ;
#8597=CARTESIAN_POINT ( 'NONE',  ( 4.132952817037849336, -4.063368025374519910, -6.938893903907228378E-15 ) ) ;
#8600=CARTESIAN_POINT ( 'NONE',  ( 4.180345472528537165, 2.086001522971432820, 3.570468649087204849 ) ) ;
#8608=CARTESIAN_POINT ( 'NONE',  ( 4.630153689607063860, -2.981509523526843174E-16, -5.371010071662830399 ) ) ;
#8629=ORIENTED_EDGE ( 'NONE', *, *, #3809, .F. ) ;
#8666=ORIENTED_EDGE ( 'NONE', *, *, #796, .T. ) ;
#8672=ORIENTED_EDGE ( 'NONE', *, *, #9151, .T. ) ;
#8673=CARTESIAN_POINT ( 'NONE',  ( 4.114405500665252013, -4.051151509359440794, -1.059651684330564515E-16 ) ) ;
#8676=CARTESIAN_POINT ( 'NONE',  ( 3.878089031707513623, 0.7015470581927707450, 3.499999999999992895 ) ) ;
#8680=AXIS2_PLACEMENT_3D ( 'NONE', #1306, #5755, #11406 ) ;
#8705=CARTESIAN_POINT ( 'NONE',  ( 4.175572532730949860, -2.061029303918042288, 3.569807470274396266 ) ) ;
#8757=VERTEX_POINT ( 'NONE', #2549 ) ;
#8760=CARTESIAN_POINT ( 'NONE',  ( 4.180345136606687717, -2.085999704580147718, -3.570468642550108207 ) ) ;
#8768=EDGE_CURVE ( 'NONE', #6636, #269, #8939, .T. ) ;
#8809=LINE ( 'NONE', #7485, #1740 ) ;
#8813=CARTESIAN_POINT ( 'NONE',  ( 4.158921614371309694, -4.076055977742311320, 0.05993604794450246853 ) ) ;
#8827=CARTESIAN_POINT ( 'NONE',  ( 4.086375874528097363, -2.103253014742902938, -3.499999999999992895 ) ) ;
#8837=CARTESIAN_POINT ( 'NONE',  ( 4.132952817037849336, 2.031684012687273722, -3.518979934899746365 ) ) ;
#8878=CARTESIAN_POINT ( 'NONE',  ( 4.052424581287747962, 2.393186648133197370, -2.990837702970422729 ) ) ;
#8882=DIRECTION ( 'NONE',  ( 1.000000000000000000, 3.286707217423839940E-17, -2.273843122241290364E-18 ) ) ;
#8888=CARTESIAN_POINT ( 'NONE',  ( 3.880206590543179512, 2.665671387532607906, 2.382921720510873254 ) ) ;
#8891=VECTOR ( 'NONE', #4590, 1000.000000000000000 ) ;
#8899=CYLINDRICAL_SURFACE ( 'NONE', #2105, 2.499999999999999112 ) ;
#8908=CARTESIAN_POINT ( 'NONE',  ( 3.948103430090705857, -2.682758828852386923, 2.353325403973848484 ) ) ;
#8911=CARTESIAN_POINT ( 'NONE',  ( 4.082498951862935321, -2.020725942163680511, 3.499999999999991118 ) ) ;
#8925=ORIENTED_EDGE ( 'NONE', *, *, #10049, .F. ) ;
#8928=ORIENTED_EDGE ( 'NONE', *, *, #13756, .T. ) ;
#8939=B_SPLINE_CURVE_WITH_KNOTS ( 'NONE', 3,
 ( #2618, #7064, #9422, #8239 ),
 .UNSPECIFIED., .F., .F.,
 ( 4, 4 ),
 ( 2.380739282110561210E-07, 0.002044882221487530176 ),
 .UNSPECIFIED. ) ;
#8942=FACE_OUTER_BOUND ( 'NONE', #3274, .T. ) ;
#8956=CARTESIAN_POINT ( 'NONE',  ( 3.951447005078477126, 2.357513599190965259, -2.916666666666663854 ) ) ;
#8957=EDGE_CURVE ( 'NONE', #8214, #13520, #6473, .T. ) ;
#8964=ADVANCED_FACE ( 'NONE', ( #7296 ), #9764, .T. ) ;
#9018=DIRECTION ( 'NONE',  ( -2.273843122241288438E-18, -5.551115123125783935E-17, -1.000000000000000000 ) ) ;
#9025=CARTESIAN_POINT ( 'NONE',  ( 3.950241966887836575, 2.668221755854076171, 2.378504353000507443 ) ) ;
#9035=CARTESIAN_POINT ( 'NONE',  ( 4.071447262713911996, 2.020725942163681399, 3.499999999999996003 ) ) ;
#9059=AXIS2_PLACEMENT_3D ( 'NONE', #13378, #8882, #2306 ) ;
#9093=CARTESIAN_POINT ( 'NONE',  ( 4.175813232069169878, 4.122719923832743660, 0.000000000000000000 ) ) ;
#9094=CARTESIAN_POINT ( 'NONE',  ( 3.973514160553474284, 3.435084588004183814, -1.181876024140317671 ) ) ;
#9096=CARTESIAN_POINT ( 'NONE',  ( 0.000000000000000000, 0.000000000000000000, 0.000000000000000000 ) ) ;
#9097=B_SPLINE_CURVE_WITH_KNOTS ( 'NONE', 3,
 ( #1053, #2293, #11142, #4442, #6603 ),
 .UNSPECIFIED., .F., .F.,
 ( 4, 1, 4 ),
 ( 0.000000000000000000, 0.002020725942163690506, 0.004041451884327381013 ),
 .UNSPECIFIED. ) ;
#9128=CARTESIAN_POINT ( 'NONE',  ( 0.3126073911696169993, -2.020725942163681399, 3.499999999999989342 ) ) ;
#9151=EDGE_CURVE ( 'NONE', #4271, #7272, #11386, .T. ) ;
#9162=CARTESIAN_POINT ( 'NONE',  ( 4.165266963751697915, 2.049631966911992009, 3.550066703508893529 ) ) ;
#9179=ORIENTED_EDGE ( 'NONE', *, *, #12406, .F. ) ;
#9215=EDGE_LOOP ( 'NONE', ( #11644, #7343 ) ) ;
#9217=EDGE_LOOP ( 'NONE', ( #9179, #12941, #9567, #12103, #8479 ) ) ;
#9236=CARTESIAN_POINT ( 'NONE',  ( 0.000000000000000000, -3.031088913245549854, -1.750000000000001554 ) ) ;
#9237=CARTESIAN_POINT ( 'NONE',  ( 4.175572532730950748, 2.061029303918053834, 3.569807470274371397 ) ) ;
#9238=ORIENTED_EDGE ( 'NONE', *, *, #11467, .T. ) ;
#9255=ADVANCED_FACE ( 'NONE', ( #10287 ), #2325, .F. ) ;
#9271=B_SPLINE_CURVE_WITH_KNOTS ( 'NONE', 3,
 ( #10487, #12471, #247, #8060, #13795, #6897, #1274, #3485, #323, #11432, #10261, #2444, #2669, #11361, #5934, #13721 ),
 .UNSPECIFIED., .F., .F.,
 ( 4, 3, 3, 3, 3, 4 ),
 ( -2.111273352609310095E-06, 0.000000000000000000, 3.519286887794623349E-05, 7.191842652066866262E-05, 0.0001049868727093422117, 0.0001382836236821615838 ),
 .UNSPECIFIED. ) ;
#9292=CARTESIAN_POINT ( 'NONE',  ( 4.071447262713911996, 4.041451884327390331, 0.000000000000000000 ) ) ;
#9303=AXIS2_PLACEMENT_3D ( 'NONE', #1065, #13447, #117 ) ;
#9326=MECHANICAL_DESIGN_GEOMETRIC_PRESENTATION_REPRESENTATION('',(#3974),#10967);
#9338=CARTESIAN_POINT ( 'NONE',  ( 4.158806752148098695, -2.089318365061883842, 3.499999999999993783 ) ) ;
#9342=EDGE_CURVE ( 'NONE', #3727, #172, #12959, .T. ) ;
#9352=CARTESIAN_POINT ( 'NONE',  ( 0.2174200650117466826, -2.185595227304854227, 3.214438021527920686 ) ) ;
#9360=EDGE_CURVE ( 'NONE', #7309, #13816, #6985, .T. ) ;
#9365=VERTEX_POINT ( 'NONE', #8303 ) ;
#9420=CARTESIAN_POINT ( 'NONE',  ( 0.3126073911695614882, -2.020725942163792421, -3.500000000000003109 ) ) ;
#9422=CARTESIAN_POINT ( 'NONE',  ( -5.360651806498819664E-15, 3.375361811986497873, -1.153701847711626982 ) ) ;
#9430=ADVANCED_FACE ( 'NONE', ( #9569 ), #12360, .F. ) ;
#9431=ORIENTED_EDGE ( 'NONE', *, *, #1170, .F. ) ;
#9443=B_SPLINE_CURVE_WITH_KNOTS ( 'NONE', 3,
 ( #6426, #8911, #3377, #11179, #1158, #13468, #10084, #76, #4549, #4266, #3439, #1984, #5335, #9798, #8705, #13734 ),
 .UNSPECIFIED., .F., .F.,
 ( 4, 3, 3, 3, 3, 4 ),
 ( 0.000000000000000000, 3.315506744709606176E-05, 6.608280158699775557E-05, 0.0001026520855291457020, 0.0001376952025664786891, 0.0001398064759190601521 ),
 .UNSPECIFIED. ) ;
#9464=CARTESIAN_POINT ( 'NONE',  ( 4.175326769692831341, 2.060699556488946538, 3.569236330973450944 ) ) ;
#9471=DIRECTION ( 'NONE',  ( 2.273843122241288438E-18, 5.551115123125782702E-17, 1.000000000000000000 ) ) ;
#9474=ORIENTED_EDGE ( 'NONE', *, *, #2893, .T. ) ;
#9491=CARTESIAN_POINT ( 'NONE',  ( 4.071447262713911996, -4.041451884327377009, 0.000000000000000000 ) ) ;
#9518=DIRECTION ( 'NONE',  ( -1.000000000000000000, -3.286707217423839940E-17, -2.273843122241288053E-18 ) ) ;
#9531=DIRECTION ( 'NONE',  ( -2.273843122241288438E-18, -5.551115123125783935E-17, -1.000000000000000000 ) ) ;
#9532=ORIENTED_EDGE ( 'NONE', *, *, #5851, .F. ) ;
#9565=CARTESIAN_POINT ( 'NONE',  ( 4.033901012035909339, 3.740908793662586884, -0.5205559028927313481 ) ) ;
#9567=ORIENTED_EDGE ( 'NONE', *, *, #11848, .T. ) ;
#9569=FACE_OUTER_BOUND ( 'NONE', #10523, .T. ) ;
#9572=DIRECTION ( 'NONE',  ( 1.000000000000000000, 3.286707217423839940E-17, 2.273843122241288053E-18 ) ) ;
#9589=ADVANCED_FACE ( 'NONE', ( #2518 ), #13290, .T. ) ;
#9606=CARTESIAN_POINT ( 'NONE',  ( 0.000000000000000000, -3.031088913245549854, -1.750000000000001554 ) ) ;
#9608=ORIENTED_EDGE ( 'NONE', *, *, #3975, .T. ) ;
#9609=EDGE_CURVE ( 'NONE', #13816, #2841, #3005, .T. ) ;
#9630=EDGE_CURVE ( 'NONE', #8264, #5579, #13654, .T. ) ;
#9637=CIRCLE ( 'NONE', #11039, 2.499999999999999112 ) ;
#9679=CARTESIAN_POINT ( 'NONE',  ( 4.071447262713911996, 2.020725942163681399, -3.499999999999996003 ) ) ;
#9687=DIRECTION ( 'NONE',  ( -1.000000000000000000, -3.286707217423839940E-17, 2.273843122241290364E-18 ) ) ;
#9690=CARTESIAN_POINT ( 'NONE',  ( 4.175572532730952524, 4.122058607836114774, -1.739027647669125673E-15 ) ) ;
#9706=B_SPLINE_CURVE_WITH_KNOTS ( 'NONE', 3,
 ( #8278, #392, #13794, #12676, #5782, #7176, #12596, #1406, #7034, #3624, #9162, #3760, #2443, #9464, #9237, #11508 ),
 .UNSPECIFIED., .F., .F.,
 ( 4, 3, 3, 3, 3, 4 ),
 ( 0.000000000000000000, 3.315506744709051878E-05, 6.608280158698574803E-05, 0.0001026520855291322985, 0.0001376952025664795836, 0.0001398064759190602334 ),
 .UNSPECIFIED. ) ;
#9760=DIRECTION ( 'NONE',  ( -1.000000000000000000, -3.286707217423839940E-17, -2.273843122241288053E-18 ) ) ;
#9764=CONICAL_SURFACE ( 'NONE', #8342, 5.371010071662830399, 1.221730476396037268 ) ;
#9766=DIRECTION ( 'NONE',  ( 0.3420201433256625512, 1.784837759418569071E-16, 0.9396926207859105373 ) ) ;
#9774=CARTESIAN_POINT ( 'NONE',  ( 4.052432342741418836, 1.393590342654194680, 3.567979436357489043 ) ) ;
#9798=CARTESIAN_POINT ( 'NONE',  ( 4.175326769692832229, -2.060699556488909678, 3.569236330973486915 ) ) ;
#9804=CARTESIAN_POINT ( 'NONE',  ( 0.02993401039713160586, 2.688325911136451030, -2.343682934607757229 ) ) ;
#9827=CIRCLE ( 'NONE', #5388, 3.499999999999999112 ) ;
#9829=AXIS2_PLACEMENT_3D ( 'NONE', #2758, #12613, #7123 ) ;
#9830=DIRECTION ( 'NONE',  ( -1.000000000000000000, -3.286707217423839940E-17, -2.273843122241288053E-18 ) ) ;
#9850=EDGE_LOOP ( 'NONE', ( #11791, #14448, #7844, #11547, #13318 ) ) ;
#9857=B_SPLINE_CURVE_WITH_KNOTS ( 'NONE', 3,
 ( #3154, #6562, #5537, #7810, #11033, #12355 ),
 .UNSPECIFIED., .F., .F.,
 ( 4, 2, 4 ),
 ( 0.000000000000000000, 0.002086519881787261485, 0.004173039763574522103 ),
 .UNSPECIFIED. ) ;
#9865=CARTESIAN_POINT ( 'NONE',  ( 3.880198502136731786, 0.7307680362939255048, -3.499999999999992895 ) ) ;
#9867=CIRCLE ( 'NONE', #12913, 5.371010071662830399 ) ;
#9876=CARTESIAN_POINT ( 'NONE',  ( 4.175075985190068728, 2.060370777630132544, -3.568666869285572307 ) ) ;
#9887=CIRCLE ( 'NONE', #4298, 3.499999999999999112 ) ;
#9921=CARTESIAN_POINT ( 'NONE',  ( 4.030867648405854098, 2.329326259789020526, -2.965488570641532373 ) ) ;
#9942=CARTESIAN_POINT ( 'NONE',  ( 4.142654963991840411, 2.035398498734362072, -3.525413613457308859 ) ) ;
#9972=CARTESIAN_POINT ( 'NONE',  ( 4.175813232069169878, -4.122719923832743660, -6.938893903907228378E-15 ) ) ;
#9993=FACE_OUTER_BOUND ( 'NONE', #5872, .T. ) ;
#9996=DIRECTION ( 'NONE',  ( -1.000000000000000000, -3.286707217423839940E-17, -2.273843122241288053E-18 ) ) ;
#10038=CARTESIAN_POINT ( 'NONE',  ( 0.3126073911696169993, -2.020725942163681399, 3.499999999999989342 ) ) ;
#10049=EDGE_CURVE ( 'NONE', #14160, #7658, #12823, .T. ) ;
#10057=CARTESIAN_POINT ( 'NONE',  ( 3.880206590543186618, -2.665671387532548398, -2.382921720511017583 ) ) ;
#10059=FACE_OUTER_BOUND ( 'NONE', #11345, .T. ) ;
#10074=CARTESIAN_POINT ( 'NONE',  ( 4.052416734886548078, -1.393505408944210266, -3.567979131523931091 ) ) ;
#10081=LINE ( 'NONE', #7584, #6569 ) ;
#10084=CARTESIAN_POINT ( 'NONE',  ( 4.132952817037849336, -2.031684012687273722, 3.518979934899753470 ) ) ;
#10095=FILL_AREA_STYLE_COLOUR ( '', #5006 ) ;
#10113=( NAMED_UNIT ( * ) SI_UNIT ( $, .STERADIAN. ) SOLID_ANGLE_UNIT ( ) );
#10130=CARTESIAN_POINT ( 'NONE',  ( 3.958484000406985004, 2.327740518748977028, -2.968235154690041178 ) ) ;
#10133=CARTESIAN_POINT ( 'NONE',  ( 4.071447262713911996, 2.020725942163681399, -3.499999999999996003 ) ) ;
#10137=DIRECTION ( 'NONE',  ( -2.273843122241288438E-18, -5.551115123125783935E-17, -1.000000000000000000 ) ) ;
#10152=DIRECTION ( 'NONE',  ( -1.000000000000000000, -3.286707217423839940E-17, -2.273843122241288053E-18 ) ) ;
#10156=CARTESIAN_POINT ( 'NONE',  ( 0.000000000000000000, 3.031088913245522320, 1.750000000000001554 ) ) ;
#10191=DIRECTION ( 'NONE',  ( 1.000000000000000000, 3.286707217423839940E-17, 2.273843122241288053E-18 ) ) ;
#10193=CARTESIAN_POINT ( 'NONE',  ( 3.951447005078473573, 3.704664227300106916, -0.5833333333333333703 ) ) ;
#10196=EDGE_CURVE ( 'NONE', #13520, #8214, #9867, .T. ) ;
#10205=AXIS2_PLACEMENT_3D ( 'NONE', #7350, #11668, #13949 ) ;
#10211=CARTESIAN_POINT ( 'NONE',  ( 0.2182387239031201021, 1.693823289467341286, -3.499999999999995115 ) ) ;
#10217=CARTESIAN_POINT ( 'NONE',  ( 0.1388410611046112797, 3.710337782248037009, 0.5735064479039858609 ) ) ;
#10219=CARTESIAN_POINT ( 'NONE',  ( 3.806834918298608539, 3.031088913245512551, 1.749999999999984679 ) ) ;
#10236=CARTESIAN_POINT ( 'NONE',  ( 0.1381419387119132147, -1.355287006778748582, 3.499999999999997335 ) ) ;
#10239=ORIENTED_EDGE ( 'NONE', *, *, #3975, .F. ) ;
#10261=CARTESIAN_POINT ( 'NONE',  ( 4.124214193018060470, -2.028338413290957210, -3.513185186763553958 ) ) ;
#10268=AXIS2_PLACEMENT_3D ( 'NONE', #6930, #1372, #8248 ) ;
#10277=ADVANCED_FACE ( 'NONE', ( #5474 ), #7031, .T. ) ;
#10287=FACE_OUTER_BOUND ( 'NONE', #2292, .T. ) ;
#10288=CARTESIAN_POINT ( 'NONE',  ( 1.151117775318593766E-15, 3.202582148906732318, 1.452965002680436379 ) ) ;
#10307=( GEOMETRIC_REPRESENTATION_CONTEXT ( 3 ) GLOBAL_UNCERTAINTY_ASSIGNED_CONTEXT ( ( #10704 ) ) GLOBAL_UNIT_ASSIGNED_CONTEXT ( ( #2803, #4910, #1616 ) ) REPRESENTATION_CONTEXT ( 'NONE', 'WORKASPACE' ) );
#10318=( GEOMETRIC_REPRESENTATION_CONTEXT ( 3 ) GLOBAL_UNCERTAINTY_ASSIGNED_CONTEXT ( ( #7332 ) ) GLOBAL_UNIT_ASSIGNED_CONTEXT ( ( #2288, #6885, #10113 ) ) REPRESENTATION_CONTEXT ( 'NONE', 'WORKASPACE' ) );
#10325=CARTESIAN_POINT ( 'NONE',  ( 5.599999999999994316, 2.020725942163681399, 3.499999999999996003 ) ) ;
#10334=EDGE_CURVE ( 'NONE', #9365, #14055, #14345, .T. ) ;
#10364=B_SPLINE_CURVE_WITH_KNOTS ( 'NONE', 3,
 ( #10970, #5342, #9804, #12016, #813, #1989 ),
 .UNSPECIFIED., .F., .F.,
 ( 4, 2, 4 ),
 ( 0.002044882221487530176, 0.003063384235218498484, 0.004081886248949466792 ),
 .UNSPECIFIED. ) ;
#10385=DIRECTION ( 'NONE',  ( 0.000000000000000000, 5.551115123125782702E-17, 1.000000000000000000 ) ) ;
#10395=ORIENTED_EDGE ( 'NONE', *, *, #9360, .F. ) ;
#10399=CARTESIAN_POINT ( 'NONE',  ( 3.973110223768753002, -0.6864646529411705389, -3.565797985667472414 ) ) ;
#10405=VERTEX_POINT ( 'NONE', #10156 ) ;
#10434=CARTESIAN_POINT ( 'NONE',  ( 0.02993401039713880149, 3.373851915354617592, 1.156317065392247878 ) ) ;
#10446=EDGE_CURVE ( 'NONE', #5579, #13171, #2533, .T. ) ;
#10487=CARTESIAN_POINT ( 'NONE',  ( 4.175813232069169878, -2.061359961916378492, -3.570380186727409200 ) ) ;
#10506=VERTEX_POINT ( 'NONE', #9420 ) ;
#10523=EDGE_LOOP ( 'NONE', ( #5322, #3672, #2119, #8629, #13261 ) ) ;
#10563=CARTESIAN_POINT ( 'NONE',  ( 4.151274195509659926, 4.079825909417491125, -1.343105029898746502E-14 ) ) ;
#10587=PRODUCT ( 'hex flange bolt small_iso_ISO 4162 - M5 x 25 x 16-N', 'hex flange bolt small_iso_ISO 4162 - M5 x 25 x 16-N', '', ( #3155 ) ) ;
#10593=EDGE_LOOP ( 'NONE', ( #9431, #5130, #13367, #2972 ) ) ;
#10600=ORIENTED_EDGE ( 'NONE', *, *, #11187, .F. ) ;
#10604=ORIENTED_EDGE ( 'NONE', *, *, #13756, .F. ) ;
#10610=ADVANCED_FACE ( 'NONE', ( #7824 ), #728, .T. ) ;
#10622=ORIENTED_EDGE ( 'NONE', *, *, #10196, .T. ) ;
#10634=ORIENTED_EDGE ( 'NONE', *, *, #4906, .F. ) ;
#10640=CARTESIAN_POINT ( 'NONE',  ( 4.175075985190124683, 4.120741555260237554, -6.938893903907228378E-15 ) ) ;
#10656=EDGE_LOOP ( 'NONE', ( #11915, #357, #3846, #10600 ) ) ;
#10661=CARTESIAN_POINT ( 'NONE',  ( 4.086262629614029862, 4.082406995609993317, 0.07093633357110699922 ) ) ;
#10679=FACE_OUTER_BOUND ( 'NONE', #9850, .T. ) ;
#10685=CARTESIAN_POINT ( 'NONE',  ( 3.880206590543183509, -3.396506438958527330, 1.117078279488994630 ) ) ;
#10704=UNCERTAINTY_MEASURE_WITH_UNIT (LENGTH_MEASURE( 1.000000000000000082E-05 ), #2803, 'distance_accuracy_value', 'NONE');
#10720=CARTESIAN_POINT ( 'NONE',  ( 3.973110223767151616, -2.262970274364543210E-11, -3.565797985667430225 ) ) ;
#10725=DIRECTION ( 'NONE',  ( -2.273843122241288438E-18, -5.551115123125783935E-17, -1.000000000000000000 ) ) ;
#10733=CARTESIAN_POINT ( 'NONE',  ( 3.974175853609984710, 3.450041667725513683, -1.156004144283957480 ) ) ;
#10736=CARTESIAN_POINT ( 'NONE',  ( 3.973110223767151616, -2.262970274364543210E-11, -3.565797985667430225 ) ) ;
#10737=ORIENTED_EDGE ( 'NONE', *, *, #8010, .F. ) ;
#10758=CIRCLE ( 'NONE', #10268, 3.499999999999999112 ) ;
#10783=VERTEX_POINT ( 'NONE', #8178 ) ;
#10816=CARTESIAN_POINT ( 'NONE',  ( 4.086262629614022757, 1.979770830881075305, 3.570936333571099297 ) ) ;
#10818=ORIENTED_EDGE ( 'NONE', *, *, #5717, .F. ) ;
#10822=DIRECTION ( 'NONE',  ( -1.000000000000000000, -3.286707217423839940E-17, -2.273843122241288053E-18 ) ) ;
#10851=FACE_OUTER_BOUND ( 'NONE', #12807, .T. ) ;
#10860=( BOUNDED_SURFACE ( )  B_SPLINE_SURFACE ( 3, 2, ( 
 ( #10661, #11908, #2843 ),
 ( #6191, #9565, #4011 ),
 ( #8458, #6257, #10733 ),
 ( #712, #10937, #4452 ),
 ( #10130, #9921, #8878 ),
 ( #6686, #7564, #12115 ) ),
 .UNSPECIFIED., .F., .F., .T. ) 
 B_SPLINE_SURFACE_WITH_KNOTS ( ( 4, 2, 4 ),
 ( 3, 3 ),
 ( 0.01651999345535504898, 0.01858032176739834312, 0.02064065007944164074 ),
 ( 0.000000000000000000, 1.000000000000000000 ),
 .UNSPECIFIED. ) 
 GEOMETRIC_REPRESENTATION_ITEM ( )  RATIONAL_B_SPLINE_SURFACE ( (
 ( 1.000000000000000000, 0.8047781103519391355, 1.000000000000000000),
 ( 1.000000000000000000, 0.8123785825601861355, 1.000000000000000000),
 ( 1.000000000000000000, 0.8190671539791591904, 1.000000000000000000),
 ( 1.000000000000000000, 0.8192352254831551939, 1.000000000000000000),
 ( 1.000000000000000000, 0.8126129677214093405, 1.000000000000000000),
 ( 1.000000000000000000, 0.8047712537969733404, 1.000000000000000000) ) ) 
 REPRESENTATION_ITEM ( '' )  SURFACE ( )  );
#10879=AXIS2_PLACEMENT_3D ( 'NONE', #6835, #10191, #13722 ) ;
#10888=B_SPLINE_CURVE_WITH_KNOTS ( 'NONE', 3,
 ( #1528, #6932, #5972, #5748, #9352, #9128 ),
 .UNSPECIFIED., .F., .F.,
 ( 4, 2, 4 ),
 ( 0.002044882221487524538, 0.003063384235218490244, 0.004081886248949456383 ),
 .UNSPECIFIED. ) ;
#10908=ORIENTED_EDGE ( 'NONE', *, *, #6598, .F. ) ;
#10928=EDGE_CURVE ( 'NONE', #13561, #13520, #8433, .T. ) ;
#10929=ADVANCED_FACE ( 'NONE', ( #4972 ), #11784, .F. ) ;
#10937=CARTESIAN_POINT ( 'NONE',  ( 3.948103430090707189, 2.682758828852394917, -2.353325403974035446 ) ) ;
#10967=( GEOMETRIC_REPRESENTATION_CONTEXT ( 3 ) GLOBAL_UNCERTAINTY_ASSIGNED_CONTEXT ( ( #759 ) ) GLOBAL_UNIT_ASSIGNED_CONTEXT ( ( #7893, #6796, #3519 ) ) REPRESENTATION_CONTEXT ( 'NONE', 'WORKASPACE' ) );
#10970=CARTESIAN_POINT ( 'NONE',  ( 0.000000000000000000, 3.031088913245536087, -1.750000000000001554 ) ) ;
#11022=CARTESIAN_POINT ( 'NONE',  ( 0.02944718078426967686, -0.6813962075686338382, -3.499999999999996891 ) ) ;
#11025=AXIS2_PLACEMENT_3D ( 'NONE', #167, #6524, #5441 ) ;
#11033=CARTESIAN_POINT ( 'NONE',  ( 4.050823680195248855, 2.400527758044911586, 2.978030508226147344 ) ) ;
#11037=CARTESIAN_POINT ( 'NONE',  ( 4.175813232069169878, 2.061359961916364725, -3.570380186727395433 ) ) ;
#11039=AXIS2_PLACEMENT_3D ( 'NONE', #5051, #9518, #603 ) ;
#11064=VERTEX_POINT ( 'NONE', #517 ) ;
#11090=CARTESIAN_POINT ( 'NONE',  ( 3.958491816110948580, 1.406739583088900236, 3.499999999999992450 ) ) ;
#11095=EDGE_CURVE ( 'NONE', #8757, #10405, #6855, .T. ) ;
#11096=CARTESIAN_POINT ( 'NONE',  ( 0.2175679805369797049, -1.691499766289379147, -3.499999999999996891 ) ) ;
#11098=FACE_OUTER_BOUND ( 'NONE', #10593, .T. ) ;
#11129=EDGE_CURVE ( 'NONE', #4092, #2047, #3215, .T. ) ;
#11137=CARTESIAN_POINT ( 'NONE',  ( 4.050536630291698970, -2.401306687817075680, 2.976670123173713822 ) ) ;
#11139=ORIENTED_EDGE ( 'NONE', *, *, #6153, .T. ) ;
#11142=CARTESIAN_POINT ( 'NONE',  ( 3.806834918298619641, -3.031088913245550298, -1.750000000000016653 ) ) ;
#11145=CARTESIAN_POINT ( 'NONE',  ( 0.3126073911696169993, -4.041451884327377009, 0.000000000000000000 ) ) ;
#11152=DIRECTION ( 'NONE',  ( 1.000000000000000000, 3.286707217423839940E-17, 2.273843122241288053E-18 ) ) ;
#11161=AXIS2_PLACEMENT_3D ( 'NONE', #12319, #3256, #4510 ) ;
#11179=CARTESIAN_POINT ( 'NONE',  ( 4.104070371397483541, -2.023683613428362005, 3.505122836902491379 ) ) ;
#11187=EDGE_CURVE ( 'NONE', #14055, #10783, #3093, .T. ) ;
#11239=ORIENTED_EDGE ( 'NONE', *, *, #5350, .T. ) ;
#11244=PRODUCT_DEFINITION ( 'UNKNOWN', '', #3836, #4288 ) ;
#11247=DIRECTION ( 'NONE',  ( 0.000000000000000000, 5.551115123125782702E-17, 1.000000000000000000 ) ) ;
#11257=B_SPLINE_CURVE_WITH_KNOTS ( 'NONE', 3,
 ( #3721, #10288, #10434, #10217, #279, #4745 ),
 .UNSPECIFIED., .F., .F.,
 ( 4, 2, 4 ),
 ( 0.002044882221487521069, 0.003063384235218490244, 0.004081886248949459853 ),
 .UNSPECIFIED. ) ;
#11262=ORIENTED_EDGE ( 'NONE', *, *, #7016, .F. ) ;
#11305=CARTESIAN_POINT ( 'NONE',  ( 4.071447262713911996, 2.020725942163681399, 3.499999999999996003 ) ) ;
#11326=( BOUNDED_SURFACE ( )  B_SPLINE_SURFACE ( 3, 2, ( 
 ( #7587, #4264, #12072 ),
 ( #2870, #1763, #6215 ),
 ( #10685, #673, #13246 ),
 ( #2329, #8908, #933 ),
 ( #7736, #7813, #12430 ),
 ( #4610, #5680, #4548 ) ),
 .UNSPECIFIED., .F., .F., .T. ) 
 B_SPLINE_SURFACE_WITH_KNOTS ( ( 4, 2, 4 ),
 ( 3, 3 ),
 ( 0.01651999345535503858, 0.01858032176739833966, 0.02064065007944164074 ),
 ( 0.000000000000000000, 1.000000000000000000 ),
 .UNSPECIFIED. ) 
 GEOMETRIC_REPRESENTATION_ITEM ( )  RATIONAL_B_SPLINE_SURFACE ( (
 ( 1.000000000000000000, 0.8047781103519388024, 1.000000000000000000),
 ( 1.000000000000000000, 0.8123785825604552535, 1.000000000000000000),
 ( 1.000000000000000000, 0.8190671539788006994, 1.000000000000000000),
 ( 1.000000000000000000, 0.8192352254835123526, 1.000000000000000000),
 ( 1.000000000000000000, 0.8126129677211405555, 1.000000000000000000),
 ( 1.000000000000000000, 0.8047712537969740065, 1.000000000000000000) ) ) 
 REPRESENTATION_ITEM ( '' )  SURFACE ( )  );
#11334=CARTESIAN_POINT ( 'NONE',  ( 5.599999999999994316, -2.020725942163681399, -3.500000000000010214 ) ) ;
#11345=EDGE_LOOP ( 'NONE', ( #13398, #2551, #1428, #4917, #10604 ) ) ;
#11361=CARTESIAN_POINT ( 'NONE',  ( 4.093692494532781723, -2.021783646005765878, -3.501831996793843160 ) ) ;
#11362=DIRECTION ( 'NONE',  ( -2.273843122241288438E-18, -5.551115123125783935E-17, -1.000000000000000000 ) ) ;
#11377=ORIENTED_EDGE ( 'NONE', *, *, #6645, .T. ) ;
#11385=EDGE_CURVE ( 'NONE', #10783, #79, #10081, .T. ) ;
#11386=LINE ( 'NONE', #349, #11632 ) ;
#11406=DIRECTION ( 'NONE',  ( 0.000000000000000000, 5.551115123125782702E-17, 1.000000000000000000 ) ) ;
#11407=( BOUNDED_SURFACE ( )  B_SPLINE_SURFACE ( 3, 2, ( 
 ( #7628, #3270, #5584 ),
 ( #12050, #2091, #13376 ),
 ( #10057, #3136, #1063 ),
 ( #2021, #909, #2304 ),
 ( #4376, #6753, #6462 ),
 ( #40, #8813, #7710 ) ),
 .UNSPECIFIED., .F., .F., .T. ) 
 B_SPLINE_SURFACE_WITH_KNOTS ( ( 4, 2, 4 ),
 ( 3, 3 ),
 ( 0.01651999345535506980, 0.01858032176739836394, 0.02064065007944165808 ),
 ( 0.000000000000000000, 1.000000000000000000 ),
 .UNSPECIFIED. ) 
 GEOMETRIC_REPRESENTATION_ITEM ( )  RATIONAL_B_SPLINE_SURFACE ( (
 ( 1.000000000000000000, 0.8047781103519401347, 1.000000000000000000),
 ( 1.000000000000000000, 0.8123785825609330935, 1.000000000000000000),
 ( 1.000000000000000000, 0.8190671539781644306, 1.000000000000000000),
 ( 1.000000000000000000, 0.8192352254841483994, 1.000000000000000000),
 ( 1.000000000000000000, 0.8126129677206640478, 1.000000000000000000),
 ( 1.000000000000000000, 0.8047712537969730073, 1.000000000000000000) ) ) 
 REPRESENTATION_ITEM ( '' )  SURFACE ( )  );
#11432=CARTESIAN_POINT ( 'NONE',  ( 4.132952817037849336, -2.031684012687273722, -3.518979934899746365 ) ) ;
#11438=DIRECTION ( 'NONE',  ( 1.000000000000000000, 3.286707217423839940E-17, 2.273843122241288053E-18 ) ) ;
#11454=CARTESIAN_POINT ( 'NONE',  ( -2.104029840979682042E-15, 0.3423821193476805358, -3.499999999999996003 ) ) ;
#11467=EDGE_CURVE ( 'NONE', #2841, #12256, #9857, .T. ) ;
#11494=ORIENTED_EDGE ( 'NONE', *, *, #6645, .F. ) ;
#11508=CARTESIAN_POINT ( 'NONE',  ( 4.175813232069169878, 2.061359961916364725, 3.570380186727388327 ) ) ;
#11536=ORIENTED_EDGE ( 'NONE', *, *, #10446, .T. ) ;
#11547=ORIENTED_EDGE ( 'NONE', *, *, #1873, .F. ) ;
#11559=EDGE_CURVE ( 'NONE', #10405, #6636, #11257, .T. ) ;
#11624=CONICAL_SURFACE ( 'NONE', #7406, 2.054999999999999716, 0.7853981633974428389 ) ;
#11625=CARTESIAN_POINT ( 'NONE',  ( 0.02944718078426632191, -0.6813962075685970898, 3.499999999999996003 ) ) ;
#11632=VECTOR ( 'NONE', #1291, 1000.000000000000000 ) ;
#11642=AXIS2_PLACEMENT_3D ( 'NONE', #4107, #13093, #12954 ) ;
#11644=ORIENTED_EDGE ( 'NONE', *, *, #13369, .T. ) ;
#11656=CARTESIAN_POINT ( 'NONE',  ( 4.175813232069169878, 4.122719923832743660, 0.000000000000000000 ) ) ;
#11668=DIRECTION ( 'NONE',  ( -2.960064101202771857E-17, -0.8660254037844380415, -0.5000000000000012212 ) ) ;
#11677=CARTESIAN_POINT ( 'NONE',  ( 4.158413352280787123, -4.089743253945648860, -1.387778780781445676E-14 ) ) ;
#11707=CARTESIAN_POINT ( 'NONE',  ( 4.175813232069169878, 2.061359961916364725, 3.570380186727388327 ) ) ;
#11739=CARTESIAN_POINT ( 'NONE',  ( 4.104070371397483541, 4.047367226856751543, -1.387778780781445676E-14 ) ) ;
#11744=CARTESIAN_POINT ( 'NONE',  ( 4.630153689607063860, -2.981509523526843174E-16, -5.371010071662830399 ) ) ;
#11746=ADVANCED_FACE ( 'NONE', ( #4858 ), #2127, .T. ) ;
#11759=DIRECTION ( 'NONE',  ( 0.000000000000000000, -5.551115123125782702E-17, -1.000000000000000000 ) ) ;
#11770=CARTESIAN_POINT ( 'NONE',  ( 4.630153689607063860, 0.000000000000000000, 0.000000000000000000 ) ) ;
#11776=TOROIDAL_SURFACE ( 'NONE', #1018, 5.200000000000001066, 0.4999999999999975020 ) ;
#11784=PLANE ( 'NONE',  #13597 ) ;
#11791=ORIENTED_EDGE ( 'NONE', *, *, #14426, .F. ) ;
#11797=CARTESIAN_POINT ( 'NONE',  ( 4.050880675075968718, 1.379097446046174458, 3.567934390854421434 ) ) ;
#11816=ORIENTED_EDGE ( 'NONE', *, *, #799, .F. ) ;
#11835=CARTESIAN_POINT ( 'NONE',  ( 4.165266963751705909, -4.099263933823995565, -1.412887983188416289E-14 ) ) ;
#11848=EDGE_CURVE ( 'NONE', #5579, #8757, #5660, .T. ) ;
#11879=EDGE_CURVE ( 'NONE', #7309, #8214, #5075, .T. ) ;
#11884=CARTESIAN_POINT ( 'NONE',  ( 0.3126073911696169993, -4.041451884327377009, 0.000000000000000000 ) ) ;
#11894=VERTEX_POINT ( 'NONE', #1562 ) ;
#11908=CARTESIAN_POINT ( 'NONE',  ( 4.158806965674307854, 4.075748668183989842, 0.05940377217583851094 ) ) ;
#11913=CARTESIAN_POINT ( 'NONE',  ( 4.071447262713911996, -2.020725942163681399, 3.499999999999989342 ) ) ;
#11915=ORIENTED_EDGE ( 'NONE', *, *, #10334, .F. ) ;
#11966=CARTESIAN_POINT ( 'NONE',  ( 0.3126073911696169993, -4.041451884327377009, 0.000000000000000000 ) ) ;
#11976=ORIENTED_EDGE ( 'NONE', *, *, #2768, .F. ) ;
#11986=EDGE_LOOP ( 'NONE', ( #4390, #771, #2538, #10634, #3517, #12176 ) ) ;
#11995=CARTESIAN_POINT ( 'NONE',  ( 0.3126073911695614882, -2.020725942163792421, -3.500000000000003109 ) ) ;
#12016=CARTESIAN_POINT ( 'NONE',  ( 0.1388410611046031196, 2.351840044243031613, -2.926493552096015360 ) ) ;
#12018=DIRECTION ( 'NONE',  ( -1.000000000000000000, -3.286707217423839940E-17, -2.273843122241288053E-18 ) ) ;
#12029=CARTESIAN_POINT ( 'NONE',  ( -5.684607805603229377E-18, 1.673838217086936480E-16, -2.499999999999999112 ) ) ;
#12033=CARTESIAN_POINT ( 'NONE',  ( 30.60000000000001563, 1.140754157802348188E-16, 2.054999999999999716 ) ) ;
#12050=CARTESIAN_POINT ( 'NONE',  ( 3.961551342853731228, -2.319461885623312458, -2.982574167880926996 ) ) ;
#12067=CARTESIAN_POINT ( 'NONE',  ( 30.60000000000001563, 0.000000000000000000, 0.000000000000000000 ) ) ;
#12072=CARTESIAN_POINT ( 'NONE',  ( 4.180231891692623769, -4.134807952925586783, -0.02076457676762514040 ) ) ;
#12085=CARTESIAN_POINT ( 'NONE',  ( 0.000000000000000000, -3.031088913245549854, -1.750000000000001554 ) ) ;
#12097=CARTESIAN_POINT ( 'NONE',  ( 3.973514160553474284, -3.435084588004187811, 1.181876024140309456 ) ) ;
#12103=ORIENTED_EDGE ( 'NONE', *, *, #1816, .F. ) ;
#12111=EDGE_LOOP ( 'NONE', ( #3456, #5313, #2020, #3798 ) ) ;
#12115=CARTESIAN_POINT ( 'NONE',  ( 4.180345304246196214, 2.049116244671346454, -3.591763845239310804 ) ) ;
#12127=DIRECTION ( 'NONE',  ( -2.273843122241289979E-18, 5.551115123125782702E-17, 1.000000000000000000 ) ) ;
#12132=LINE ( 'NONE', #1079, #8156 ) ;
#12147=ORIENTED_EDGE ( 'NONE', *, *, #1999, .T. ) ;
#12150=CARTESIAN_POINT ( 'NONE',  ( 30.60000000000001563, 0.000000000000000000, 0.000000000000000000 ) ) ;
#12176=ORIENTED_EDGE ( 'NONE', *, *, #12976, .F. ) ;
#12191=CARTESIAN_POINT ( 'NONE',  ( 3.948095570617038419, 0.6965071952232524399, 3.499999999999992895 ) ) ;
#12198=CARTESIAN_POINT ( 'NONE',  ( 4.055492966679574707, 2.385006769472713728, 3.005124364834414141 ) ) ;
#12238=CARTESIAN_POINT ( 'NONE',  ( 0.1217565302851009168, -2.351289329882169987, -2.927447417349498426 ) ) ;
#12247=CARTESIAN_POINT ( 'NONE',  ( 0.000000000000000000, 0.000000000000000000, 0.000000000000000000 ) ) ;
#12256=VERTEX_POINT ( 'NONE', #11707 ) ;
#12272=CARTESIAN_POINT ( 'NONE',  ( 3.948103430091011834, 3.379418997638845124, 1.146674596025581527 ) ) ;
#12285=CARTESIAN_POINT ( 'NONE',  ( 30.60000000000001563, 1.375895014445462134E-16, -2.054999999999999716 ) ) ;
#12315=DIRECTION ( 'NONE',  ( 2.273843122241288438E-18, 5.551115123125783935E-17, 1.000000000000000000 ) ) ;
#12316=CARTESIAN_POINT ( 'NONE',  ( 3.973514160553477836, -2.741076955031354956, -2.383932505289875881 ) ) ;
#12319=CARTESIAN_POINT ( 'NONE',  ( 0.000000000000000000, 0.000000000000000000, 0.000000000000000000 ) ) ;
#12335=DIRECTION ( 'NONE',  ( -2.273843122241288438E-18, -5.551115123125783935E-17, -1.000000000000000000 ) ) ;
#12339=CARTESIAN_POINT ( 'NONE',  ( 3.974175853610007358, 2.726149789692824399, 2.409821656223152697 ) ) ;
#12348=FACE_OUTER_BOUND ( 'NONE', #3130, .T. ) ;
#12355=CARTESIAN_POINT ( 'NONE',  ( 4.175813232069169878, 2.061359961916364725, 3.570380186727388327 ) ) ;
#12360=( BOUNDED_SURFACE ( )  B_SPLINE_SURFACE ( 3, 2, ( 
 ( #8464, #9338, #2928 ),
 ( #3795, #7424, #4380 ),
 ( #4315, #14118, #4238 ),
 ( #8676, #12191, #790 ),
 ( #11090, #13020, #9774 ),
 ( #2094, #2172, #8600 ) ),
 .UNSPECIFIED., .F., .F., .T. ) 
 B_SPLINE_SURFACE_WITH_KNOTS ( ( 4, 2, 4 ),
 ( 3, 3 ),
 ( 0.01651732063679902870, 0.01857756227444015348, 0.02063780391208127826 ),
 ( 0.000000000000000000, 1.000000000000000000 ),
 .UNSPECIFIED. ) 
 GEOMETRIC_REPRESENTATION_ITEM ( )  RATIONAL_B_SPLINE_SURFACE ( (
 ( 1.000000000000000000, 0.8047781231227495446, 1.000000000000000000),
 ( 1.000000000000000000, 0.8123782108664119317, 1.000000000000000000),
 ( 1.000000000000000000, 0.8190665102134654374, 1.000000000000000000),
 ( 1.000000000000000000, 0.8192358432842802296, 1.000000000000000000),
 ( 1.000000000000000000, 0.8126132624436200880, 1.000000000000000000),
 ( 1.000000000000000000, 0.8047712436238865230, 1.000000000000000000) ) ) 
 REPRESENTATION_ITEM ( '' )  SURFACE ( )  );
#12387=ADVANCED_FACE ( 'NONE', ( #7518 ), #11326, .F. ) ;
#12389=ORIENTED_EDGE ( 'NONE', *, *, #7441, .T. ) ;
#12399=FACE_OUTER_BOUND ( 'NONE', #4325, .T. ) ;
#12406=EDGE_CURVE ( 'NONE', #8264, #4092, #4545, .T. ) ;
#12412=AXIS2_PLACEMENT_3D ( 'NONE', #12150, #12018, #6577 ) ;
#12419=CARTESIAN_POINT ( 'NONE',  ( 4.086262841041381932, 2.102637316508702447, -3.499999999999992450 ) ) ;
#12429=CARTESIAN_POINT ( 'NONE',  ( 3.951447005078475350, 3.704664227300108692, 0.5833333333333335924 ) ) ;
#12430=CARTESIAN_POINT ( 'NONE',  ( 4.052424581287699112, -2.393186648133069916, 2.990837702970342349 ) ) ;
#12459=EDGE_CURVE ( 'NONE', #13816, #14126, #8072, .T. ) ;
#12471=CARTESIAN_POINT ( 'NONE',  ( 4.175572532730949860, -2.061029303918050282, -3.569807470274399375 ) ) ;
#12474=FACE_OUTER_BOUND ( 'NONE', #11986, .T. ) ;
#12493=DIRECTION ( 'NONE',  ( -3.286707217423840556E-17, -1.000000000000000000, -2.220446049250313574E-16 ) ) ;
#12533=CARTESIAN_POINT ( 'NONE',  ( 3.806834918298616088, 3.031088913245548966, -1.750000000000005551 ) ) ;
#12571=SURFACE_STYLE_USAGE ( .BOTH. , #3664 ) ;
#12574=CARTESIAN_POINT ( 'NONE',  ( 0.000000000000000000, 3.031088913245522320, 1.750000000000001554 ) ) ;
#12596=CARTESIAN_POINT ( 'NONE',  ( 4.132952817037849336, 2.031684012687246188, 3.518979934899739259 ) ) ;
#12613=DIRECTION ( 'NONE',  ( -3.286707217423839940E-17, 1.000000000000000000, 6.695352868347748137E-17 ) ) ;
#12644=B_SPLINE_CURVE_WITH_KNOTS ( 'NONE', 3,
 ( #9606, #13138, #624, #7334, #822, #11884 ),
 .UNSPECIFIED., .F., .F.,
 ( 4, 2, 4 ),
 ( 0.002044882221487529742, 0.003063384235218501520, 0.004081886248949473731 ),
 .UNSPECIFIED. ) ;
#12662=FILL_AREA_STYLE_COLOUR ( '', #6097 ) ;
#12663=EDGE_LOOP ( 'NONE', ( #8928, #841, #9608 ) ) ;
#12676=CARTESIAN_POINT ( 'NONE',  ( 4.104070371397483541, 2.023683613428362005, 3.505122836902505146 ) ) ;
#12807=EDGE_LOOP ( 'NONE', ( #6729, #1929, #7937, #13150 ) ) ;
#12823=B_SPLINE_CURVE_WITH_KNOTS ( 'NONE', 3,
 ( #1533, #6745, #1118, #12316, #7774, #3331 ),
 .UNSPECIFIED., .F., .F.,
 ( 4, 2, 4 ),
 ( 0.000000000000000000, 0.002086519881787259750, 0.004173039763574519501 ),
 .UNSPECIFIED. ) ;
#12836=CARTESIAN_POINT ( 'NONE',  ( 4.071447262713911996, 4.041451884327390331, 0.000000000000000000 ) ) ;
#12839=FACE_OUTER_BOUND ( 'NONE', #4815, .T. ) ;
#12870=CARTESIAN_POINT ( 'NONE',  ( 0.000000000000000000, 3.031088913245536087, -1.750000000000001554 ) ) ;
#12913=AXIS2_PLACEMENT_3D ( 'NONE', #7447, #1832, #14138 ) ;
#12915=DIRECTION ( 'NONE',  ( -1.000000000000000000, -3.286707217423839940E-17, -2.273843122241288053E-18 ) ) ;
#12919=ORIENTED_EDGE ( 'NONE', *, *, #1999, .F. ) ;
#12941=ORIENTED_EDGE ( 'NONE', *, *, #9630, .T. ) ;
#12954=DIRECTION ( 'NONE',  ( -2.273843122241288438E-18, -5.551115123125783935E-17, -1.000000000000000000 ) ) ;
#12959=B_SPLINE_CURVE_WITH_KNOTS ( 'NONE', 3,
 ( #7364, #14048, #13962, #5094 ),
 .UNSPECIFIED., .F., .F.,
 ( 4, 4 ),
 ( 0.002080789711329273685, 0.004173039763574509092 ),
 .UNSPECIFIED. ) ;
#12969=DIRECTION ( 'NONE',  ( 3.286707217423839940E-17, -1.000000000000000000, 5.551115123125782702E-17 ) ) ;
#12976=EDGE_CURVE ( 'NONE', #269, #10405, #5647, .T. ) ;
#13020=CARTESIAN_POINT ( 'NONE',  ( 4.030875481282749639, 1.403567514398344596, 3.499999999999992006 ) ) ;
#13066=CARTESIAN_POINT ( 'NONE',  ( 4.082498951862935321, 4.041451884327390331, 2.512980736064700723E-20 ) ) ;
#13084=CARTESIAN_POINT ( 'NONE',  ( 4.093692494532779946, -4.043567292011558401, 1.064034557724744967E-16 ) ) ;
#13093=DIRECTION ( 'NONE',  ( 1.000000000000000000, 3.286707217423839940E-17, 2.273843122241288053E-18 ) ) ;
#13138=CARTESIAN_POINT ( 'NONE',  ( -2.976897293125237753E-15, -3.202582148906733206, -1.452965002680418616 ) ) ;
#13149=LINE ( 'NONE', #776, #7289 ) ;
#13150=ORIENTED_EDGE ( 'NONE', *, *, #8957, .F. ) ;
#13151=DIRECTION ( 'NONE',  ( 0.000000000000000000, 5.551115123125782702E-17, 1.000000000000000000 ) ) ;
#13153=DIRECTION ( 'NONE',  ( 1.000000000000000000, 3.286707217423839940E-17, 2.273843122241288053E-18 ) ) ;
#13167=B_SPLINE_CURVE_WITH_KNOTS ( 'NONE', 3,
 ( #2610, #10211, #8012, #6983, #11454, #1514 ),
 .UNSPECIFIED., .F., .F.,
 ( 4, 2, 4 ),
 ( 0.01103795673506155484, 0.01206113197427181871, 0.01308430721348208085 ),
 .UNSPECIFIED. ) ;
#13171=VERTEX_POINT ( 'NONE', #9292 ) ;
#13179=DIRECTION ( 'NONE',  ( 0.000000000000000000, 5.551115123125782702E-17, 1.000000000000000000 ) ) ;
#13181=DIRECTION ( 'NONE',  ( -1.000000000000000000, -3.286707217423839940E-17, -2.273843122241288053E-18 ) ) ;
#13235=ORIENTED_EDGE ( 'NONE', *, *, #11095, .F. ) ;
#13245=DIRECTION ( 'NONE',  ( 1.000000000000000000, 3.286707217423839940E-17, 2.273843122241288053E-18 ) ) ;
#13246=CARTESIAN_POINT ( 'NONE',  ( 3.974175853610038445, -3.450041667725644690, 1.156004144284026758 ) ) ;
#13261=ORIENTED_EDGE ( 'NONE', *, *, #9630, .F. ) ;
#13264=AXIS2_PLACEMENT_3D ( 'NONE', #5859, #3765, #9471 ) ;
#13290=CONICAL_SURFACE ( 'NONE', #2531, 3.499999999999999112, 1.047197551196600296 ) ;
#13292=CARTESIAN_POINT ( 'NONE',  ( 4.071447262713911996, 2.020725942163681399, -3.499999999999996003 ) ) ;
#13293=CARTESIAN_POINT ( 'NONE',  ( 3.973110223767151616, 2.262797354954571809E-11, 3.565797985667430225 ) ) ;
#13309=CARTESIAN_POINT ( 'NONE',  ( 4.158921444904712494, -2.089933220600059371, -3.499999999999992895 ) ) ;
#13317=CARTESIAN_POINT ( 'NONE',  ( 4.124214193018061358, 2.028338413290956765, -3.513185186763553070 ) ) ;
#13318=ORIENTED_EDGE ( 'NONE', *, *, #8768, .F. ) ;
#13359=ORIENTED_EDGE ( 'NONE', *, *, #10049, .T. ) ;
#13367=ORIENTED_EDGE ( 'NONE', *, *, #11385, .T. ) ;
#13369=EDGE_CURVE ( 'NONE', #79, #6673, #9637, .T. ) ;
#13376=CARTESIAN_POINT ( 'NONE',  ( 4.055492966679507205, -2.385006769472553856, -3.005124364834288908 ) ) ;
#13378=CARTESIAN_POINT ( 'NONE',  ( 0.000000000000000000, 4.041451884327390331, 0.000000000000000000 ) ) ;
#13379=DIRECTION ( 'NONE',  ( 1.000000000000000000, 3.286707217423839940E-17, 2.273843122241288053E-18 ) ) ;
#13386=CARTESIAN_POINT ( 'NONE',  ( 4.180345304246193550, 4.135116856707387711, -0.02129519942690456108 ) ) ;
#13390=AXIS2_PLACEMENT_3D ( 'NONE', #14245, #1952, #11759 ) ;
#13392=CARTESIAN_POINT ( 'NONE',  ( 3.878104551856469850, -0.7018542299766717951, -3.499999999999992895 ) ) ;
#13398=ORIENTED_EDGE ( 'NONE', *, *, #9151, .F. ) ;
#13447=DIRECTION ( 'NONE',  ( 1.000000000000000000, 3.286707217423839940E-17, 2.273843122241288053E-18 ) ) ;
#13454=ORIENTED_EDGE ( 'NONE', *, *, #6273, .F. ) ;
#13460=CARTESIAN_POINT ( 'NONE',  ( 3.948111298834958482, -0.6968132764982380989, -3.499999999999837019 ) ) ;
#13468=CARTESIAN_POINT ( 'NONE',  ( 4.124214193018059582, -2.028338413290955877, 3.513185186763558843 ) ) ;
#13477=PRESENTATION_STYLE_ASSIGNMENT (( #12571 ) ) ;
#13507=CARTESIAN_POINT ( 'NONE',  ( 3.806834918298612536, -3.031088913245542305, 1.750000000000002442 ) ) ;
#13511=CARTESIAN_POINT ( 'NONE',  ( 4.071447262713911996, 4.041451884327390331, 0.000000000000000000 ) ) ;
#13512=CARTESIAN_POINT ( 'NONE',  ( 4.175813232069169878, 4.122719923832743660, 0.000000000000000000 ) ) ;
#13516=CARTESIAN_POINT ( 'NONE',  ( 4.033901012036112732, 2.321269032828268131, 2.979444097106787481 ) ) ;
#13520=VERTEX_POINT ( 'NONE', #6711 ) ;
#13556=CIRCLE ( 'NONE', #8391, 2.054999999999999716 ) ;
#13561=VERTEX_POINT ( 'NONE', #5479 ) ;
#13565=PLANE ( 'NONE',  #1296 ) ;
#13571=EDGE_CURVE ( 'NONE', #8264, #172, #9443, .T. ) ;
#13597=AXIS2_PLACEMENT_3D ( 'NONE', #14063, #5111, #3014 ) ;
#13644=CARTESIAN_POINT ( 'NONE',  ( 3.973110223767151616, -2.262970274364543210E-11, -3.565797985667430225 ) ) ;
#13654=B_SPLINE_CURVE_WITH_KNOTS ( 'NONE', 3,
 ( #119, #6900, #3351, #2243, #11305 ),
 .UNSPECIFIED., .F., .F.,
 ( 4, 1, 4 ),
 ( 0.000000000000000000, 0.002020725942163686603, 0.004041451884327373206 ),
 .UNSPECIFIED. ) ;
#13660=EDGE_CURVE ( 'NONE', #2270, #1103, #9887, .T. ) ;
#13689=CARTESIAN_POINT ( 'NONE',  ( 4.093692494532781723, 2.021783646005765878, -3.501831996793842272 ) ) ;
#13694=CARTESIAN_POINT ( 'NONE',  ( 5.599999999999994316, 0.000000000000000000, 0.000000000000000000 ) ) ;
#13695=SURFACE_STYLE_FILL_AREA ( #5622 ) ;
#13721=CARTESIAN_POINT ( 'NONE',  ( 4.071447262713911996, -2.020725942163681399, -3.500000000000010214 ) ) ;
#13722=DIRECTION ( 'NONE',  ( -2.273843122241288438E-18, -5.551115123125783935E-17, -1.000000000000000000 ) ) ;
#13734=CARTESIAN_POINT ( 'NONE',  ( 4.175813232069169878, -2.061359961916364725, 3.570380186727409200 ) ) ;
#13756=EDGE_CURVE ( 'NONE', #7272, #2270, #3334, .T. ) ;
#13794=CARTESIAN_POINT ( 'NONE',  ( 4.093692494532780835, 2.021783646005765878, 3.501831996793842716 ) ) ;
#13795=CARTESIAN_POINT ( 'NONE',  ( 4.170895651974821483, -2.054890354522748375, -3.559174498016296706 ) ) ;
#13798=CARTESIAN_POINT ( 'NONE',  ( 30.15499999999998693, 0.000000000000000000, 0.000000000000000000 ) ) ;
#13816=VERTEX_POINT ( 'NONE', #1269 ) ;
#13872=DIRECTION ( 'NONE',  ( -0.7071067811865513475, 1.601178185494237639E-17, 0.7071067811865435759 ) ) ;
#13926=CARTESIAN_POINT ( 'NONE',  ( 3.973110223768752114, 0.6864646529411640996, 3.565797985667471970 ) ) ;
#13938=CARTESIAN_POINT ( 'NONE',  ( 4.124214193018064911, 4.056676826581889550, -6.846764070645731666E-15 ) ) ;
#13949=DIRECTION ( 'NONE',  ( 1.446433017903778039E-17, 0.5000000000000012212, -0.8660254037844380415 ) ) ;
#13962=CARTESIAN_POINT ( 'NONE',  ( 4.050480423730761004, -1.376911654797407403, 3.567926555162034941 ) ) ;
#14048=CARTESIAN_POINT ( 'NONE',  ( 3.973110223765541793, -0.6902454861566503785, 3.565797985667388481 ) ) ;
#14051=DIRECTION ( 'NONE',  ( 0.000000000000000000, -5.551115123125782702E-17, -1.000000000000000000 ) ) ;
#14055=VERTEX_POINT ( 'NONE', #4286 ) ;
#14063=CARTESIAN_POINT ( 'NONE',  ( 5.599999999999994316, -2.020725942163681399, -3.500000000000010214 ) ) ;
#14104=CIRCLE ( 'NONE', #7770, 5.200000000000001066 ) ;
#14111=ORIENTED_EDGE ( 'NONE', *, *, #3641, .F. ) ;
#14115=CARTESIAN_POINT ( 'NONE',  ( 4.104070371397483541, -4.047367226856751543, 0.000000000000000000 ) ) ;
#14118=CARTESIAN_POINT ( 'NONE',  ( 3.950250160040158942, -0.7258013381033927569, 3.499999999999992895 ) ) ;
#14123=ORIENTED_EDGE ( 'NONE', *, *, #12976, .T. ) ;
#14126=VERTEX_POINT ( 'NONE', #9679 ) ;
#14129=ORIENTED_EDGE ( 'NONE', *, *, #9609, .F. ) ;
#14132=CARTESIAN_POINT ( 'NONE',  ( 5.599999999999994316, 2.020725942163681399, -3.499999999999996003 ) ) ;
#14138=DIRECTION ( 'NONE',  ( 0.000000000000000000, 5.551115123125782702E-17, 1.000000000000000000 ) ) ;
#14160=VERTEX_POINT ( 'NONE', #1782 ) ;
#14235=ORIENTED_EDGE ( 'NONE', *, *, #1381, .T. ) ;
#14245=CARTESIAN_POINT ( 'NONE',  ( 5.599999999999994316, 0.000000000000000000, 0.000000000000000000 ) ) ;
#14345=LINE ( 'NONE', #12285, #8421 ) ;
#14346=CARTESIAN_POINT ( 'NONE',  ( 4.170895651974821483, 2.054890354522617812, -3.559174498016382859 ) ) ;
#14393=FACE_OUTER_BOUND ( 'NONE', #2645, .T. ) ;
#14426=EDGE_CURVE ( 'NONE', #13171, #6636, #13149, .T. ) ;
#14445=CONICAL_SURFACE ( 'NONE', #11161, 3.499999999999999112, 1.047197551196600296 ) ;
#14448=ORIENTED_EDGE ( 'NONE', *, *, #2768, .T. ) ;
#14462=CARTESIAN_POINT ( 'NONE',  ( 4.175813232069169878, 2.061359961916364725, -3.570380186727395433 ) ) ;
ENDSEC;
END-ISO-10303-21;
